ISO-10303-21;
HEADER;
/* Generated by software containing ST-Developer
 * from STEP Tools, Inc. (www.steptools.com) 
 */

FILE_DESCRIPTION(
/* description */ ('Pipe clamp stand with threaded column'),
/* implementation_level */ '2;1');

FILE_NAME(
/* name */ 'M24 adjustment nut (3).step',
/* time_stamp */ '2026-10-27T10:55:48-07:00',
/* author */ (''),
/* organization */ (''),
/* preprocessor_version */ 'ST-DEVELOPER v20.2',
/* originating_system */ 'Autodesk Translation Framework v15.17.0.0',
/* authorisation */ '');

FILE_SCHEMA (('AUTOMOTIVE_DESIGN { 1 0 10303 214 3 1 1 }'));
ENDSEC;

DATA;
#10=MECHANICAL_DESIGN_GEOMETRIC_PRESENTATION_REPRESENTATION('',(#770),#34433);
#215=B_SPLINE_SURFACE_WITH_KNOTS('',3,3,((#33463,#33464,#33465,#33466,#33467,
#33468,#33469,#33470,#33471,#33472,#33473,#33474,#33475,#33476,#33477,#33478,
#33479,#33480,#33481,#33482,#33483,#33484,#33485,#33486,#33487,#33488,#33489,
#33490,#33491,#33492,#33493,#33494,#33495,#33496,#33497,#33498,#33499,#33500,
#33501,#33502,#33503,#33504,#33505,#33506,#33507,#33508,#33509,#33510,#33511,
#33512,#33513,#33514,#33515,#33516,#33517,#33518,#33519,#33520,#33521),
(#33522,#33523,#33524,#33525,#33526,#33527,#33528,#33529,#33530,#33531,
#33532,#33533,#33534,#33535,#33536,#33537,#33538,#33539,#33540,#33541,#33542,
#33543,#33544,#33545,#33546,#33547,#33548,#33549,#33550,#33551,#33552,#33553,
#33554,#33555,#33556,#33557,#33558,#33559,#33560,#33561,#33562,#33563,#33564,
#33565,#33566,#33567,#33568,#33569,#33570,#33571,#33572,#33573,#33574,#33575,
#33576,#33577,#33578,#33579,#33580),(#33581,#33582,#33583,#33584,#33585,
#33586,#33587,#33588,#33589,#33590,#33591,#33592,#33593,#33594,#33595,#33596,
#33597,#33598,#33599,#33600,#33601,#33602,#33603,#33604,#33605,#33606,#33607,
#33608,#33609,#33610,#33611,#33612,#33613,#33614,#33615,#33616,#33617,#33618,
#33619,#33620,#33621,#33622,#33623,#33624,#33625,#33626,#33627,#33628,#33629,
#33630,#33631,#33632,#33633,#33634,#33635,#33636,#33637,#33638,#33639),
(#33640,#33641,#33642,#33643,#33644,#33645,#33646,#33647,#33648,#33649,
#33650,#33651,#33652,#33653,#33654,#33655,#33656,#33657,#33658,#33659,#33660,
#33661,#33662,#33663,#33664,#33665,#33666,#33667,#33668,#33669,#33670,#33671,
#33672,#33673,#33674,#33675,#33676,#33677,#33678,#33679,#33680,#33681,#33682,
#33683,#33684,#33685,#33686,#33687,#33688,#33689,#33690,#33691,#33692,#33693,
#33694,#33695,#33696,#33697,#33698)),.UNSPECIFIED.,.F.,.F.,.F.,(4,4),(4,
1,1,1,1,1,1,1,1,1,1,1,1,1,1,1,1,1,1,1,1,1,1,1,1,1,1,1,1,1,1,1,1,1,1,1,1,
1,1,1,1,1,1,1,1,1,1,1,1,1,1,1,1,1,1,1,4),(0.,0.193239135097767),(11.852035964745,
12.3369705490203,12.8219051332955,13.3068397175708,13.7917743018461,14.2767088861214,
14.7616434703967,15.2465780546719,15.7315126389472,16.2164472232225,16.7013818074978,
17.1863163917731,17.6712509760483,18.1561855603236,18.6411201445989,19.1260547288742,
19.6109893131494,20.0959238974247,20.5808584817,21.0657930659753,21.5507276502506,
22.0356622345258,22.5205968188011,23.0055314030764,23.4904659873517,23.9754005716269,
24.4603351559022,24.9452697401775,25.4302043244528,25.9151389087281,26.4000734930033,
26.8850080772786,27.3699426615539,27.8548772458292,28.3398118301045,28.8247464143797,
29.309680998655,29.7946155829303,30.2795501672056,30.7644847514808,31.2494193357561,
31.7343539200314,32.2192885043067,32.704223088582,33.1891576728572,33.6740922571325,
34.1590268414078,34.6439614256831,35.1288960099583,35.6138305942336,36.0987651785089,
36.5836997627842,37.0686343470595,37.5535689313347,38.03850351561,38.5234380998853,
39.0083726841606),.UNSPECIFIED.);
#216=B_SPLINE_SURFACE_WITH_KNOTS('',3,3,((#33897,#33898,#33899,#33900,#33901,
#33902,#33903,#33904,#33905,#33906,#33907,#33908,#33909,#33910,#33911,#33912,
#33913,#33914,#33915,#33916,#33917,#33918,#33919,#33920,#33921,#33922,#33923,
#33924,#33925,#33926,#33927,#33928,#33929,#33930,#33931,#33932,#33933,#33934,
#33935,#33936,#33937,#33938,#33939,#33940,#33941,#33942,#33943,#33944,#33945,
#33946,#33947,#33948,#33949,#33950,#33951,#33952,#33953,#33954,#33955),
(#33956,#33957,#33958,#33959,#33960,#33961,#33962,#33963,#33964,#33965,
#33966,#33967,#33968,#33969,#33970,#33971,#33972,#33973,#33974,#33975,#33976,
#33977,#33978,#33979,#33980,#33981,#33982,#33983,#33984,#33985,#33986,#33987,
#33988,#33989,#33990,#33991,#33992,#33993,#33994,#33995,#33996,#33997,#33998,
#33999,#34000,#34001,#34002,#34003,#34004,#34005,#34006,#34007,#34008,#34009,
#34010,#34011,#34012,#34013,#34014),(#34015,#34016,#34017,#34018,#34019,
#34020,#34021,#34022,#34023,#34024,#34025,#34026,#34027,#34028,#34029,#34030,
#34031,#34032,#34033,#34034,#34035,#34036,#34037,#34038,#34039,#34040,#34041,
#34042,#34043,#34044,#34045,#34046,#34047,#34048,#34049,#34050,#34051,#34052,
#34053,#34054,#34055,#34056,#34057,#34058,#34059,#34060,#34061,#34062,#34063,
#34064,#34065,#34066,#34067,#34068,#34069,#34070,#34071,#34072,#34073),
(#34074,#34075,#34076,#34077,#34078,#34079,#34080,#34081,#34082,#34083,
#34084,#34085,#34086,#34087,#34088,#34089,#34090,#34091,#34092,#34093,#34094,
#34095,#34096,#34097,#34098,#34099,#34100,#34101,#34102,#34103,#34104,#34105,
#34106,#34107,#34108,#34109,#34110,#34111,#34112,#34113,#34114,#34115,#34116,
#34117,#34118,#34119,#34120,#34121,#34122,#34123,#34124,#34125,#34126,#34127,
#34128,#34129,#34130,#34131,#34132)),.UNSPECIFIED.,.F.,.F.,.F.,(4,4),(4,
1,1,1,1,1,1,1,1,1,1,1,1,1,1,1,1,1,1,1,1,1,1,1,1,1,1,1,1,1,1,1,1,1,1,1,1,
1,1,1,1,1,1,1,1,1,1,1,1,1,1,1,1,1,1,1,4),(0.,0.193239135097767),(14.3987024268659,
14.8836370111412,15.3685715954165,15.8535061796917,16.338440763967,16.8233753482423,
17.3083099325176,17.7932445167929,18.2781791010681,18.7631136853434,19.2480482696187,
19.732982853894,20.2179174381693,20.7028520224445,21.1877866067198,21.6727211909951,
22.1576557752704,22.6425903595456,23.1275249438209,23.6124595280962,24.0973941123715,
24.5823286966468,25.067263280922,25.5521978651973,26.0371324494726,26.5220670337479,
27.0070016180232,27.4919362022984,27.9768707865737,28.461805370849,28.9467399551243,
29.4316745393995,29.9166091236748,30.4015437079501,30.8864782922254,31.3714128765007,
31.8563474607759,32.3412820450512,32.8262166293265,33.3111512136018,33.7960857978771,
34.2810203821523,34.7659549664276,35.2508895507029,35.7358241349782,36.2207587192535,
36.7056933035287,37.190627887804,37.6755624720793,38.1604970563546,38.6454316406298,
39.1303662249051,39.6153008091804,40.1002353934557,40.585169977731,41.0701045620062,
41.5550391462815),.UNSPECIFIED.);
#673=B_SPLINE_CURVE_WITH_KNOTS('',3,(#33021,#33022,#33023,#33024,#33025,
#33026,#33027),.UNSPECIFIED.,.F.,.F.,(4,3,4),(26.4420020698014,26.6714021351403,
27.1563367194156),.UNSPECIFIED.);
#674=B_SPLINE_CURVE_WITH_KNOTS('',3,(#33030,#33031,#33032,#33033,#33034,
#33035,#33036,#33037,#33038,#33039,#33040,#33041,#33042,#33043,#33044,#33045,
#33046,#33047,#33048),.UNSPECIFIED.,.F.,.F.,(4,3,3,3,3,3,4),(-25.1327412287183,
-24.7316637980392,-24.2467292137639,-23.7617946294886,-23.2768600452134,
-22.7919254609381,-22.7054832247428),.UNSPECIFIED.);
#675=B_SPLINE_CURVE_WITH_KNOTS('',3,(#33053,#33054,#33055,#33056,#33057,
#33058,#33059,#33060,#33061,#33062,#33063,#33064,#33065,#33066,#33067,#33068,
#33069,#33070,#33071,#33072,#33073,#33074,#33075,#33076,#33077,#33078,#33079,
#33080,#33081,#33082,#33083,#33084,#33085,#33086,#33087,#33088,#33089,#33090,
#33091,#33092,#33093,#33094,#33095),.UNSPECIFIED.,.F.,.F.,(4,3,3,3,3,3,
3,3,3,3,3,3,3,3,4),(20.1588167626218,20.3672525395617,20.852187123837,21.3371217081123,
21.8220562923875,22.3069908766628,22.7919254609381,23.2768600452134,23.7617946294887,
24.2467292137639,24.7316637980392,25.2165983823145,25.7015329665898,26.1864675508651,
26.4420020698014),.UNSPECIFIED.);
#676=B_SPLINE_CURVE_WITH_KNOTS('',3,(#33096,#33097,#33098,#33099,#33100,
#33101,#33102,#33103,#33104,#33105,#33106,#33107,#33108,#33109,#33110,#33111,
#33112,#33113,#33114,#33115,#33116,#33117,#33118,#33119,#33120,#33121,#33122,
#33123,#33124,#33125,#33126,#33127,#33128,#33129,#33130,#33131,#33132,#33133,
#33134,#33135,#33136,#33137,#33138),.UNSPECIFIED.,.F.,.F.,(4,3,3,3,3,3,
3,3,3,3,3,3,3,3,4),(-22.7054832247428,-22.3069908766628,-21.8220562923875,
-21.3371217081122,-20.852187123837,-20.3672525395617,-19.8823179552864,
-19.3973833710111,-18.9124487867359,-18.4275142024606,-17.9425796181853,
-17.45764503391,-16.9727104496347,-16.4877758653595,-16.4222979175632),
 .UNSPECIFIED.);
#677=B_SPLINE_CURVE_WITH_KNOTS('',3,(#33143,#33144,#33145,#33146,#33147,
#33148,#33149,#33150,#33151,#33152,#33153,#33154,#33155,#33156,#33157,#33158,
#33159,#33160,#33161,#33162,#33163,#33164,#33165,#33166,#33167,#33168,#33169,
#33170,#33171,#33172,#33173,#33174,#33175,#33176,#33177,#33178,#33179,#33180,
#33181,#33182,#33183,#33184,#33185),.UNSPECIFIED.,.F.,.F.,(4,3,3,3,3,3,
3,3,3,3,3,3,3,3,4),(13.8756314554422,14.0631029439831,14.5480375282584,
15.0329721125336,15.5179066968089,16.0028412810842,16.4877758653595,16.9727104496348,
17.45764503391,17.9425796181853,18.4275142024606,18.9124487867359,19.3973833710111,
19.8823179552864,20.1588167626218),.UNSPECIFIED.);
#678=B_SPLINE_CURVE_WITH_KNOTS('',3,(#33186,#33187,#33188,#33189,#33190,
#33191,#33192,#33193,#33194,#33195,#33196,#33197,#33198,#33199,#33200,#33201,
#33202,#33203,#33204,#33205,#33206,#33207,#33208,#33209,#33210,#33211,#33212,
#33213,#33214,#33215,#33216,#33217,#33218,#33219,#33220,#33221,#33222,#33223,
#33224,#33225,#33226,#33227,#33228),.UNSPECIFIED.,.F.,.F.,(4,3,3,3,3,3,
3,3,3,3,3,3,3,3,4),(-16.4222979175632,-16.0028412810842,-15.5179066968089,
-15.0329721125336,-14.5480375282584,-14.0631029439831,-13.5781683597078,
-13.0932337754325,-12.6082991911572,-12.123364606882,-11.6384300226067,
-11.1534954383314,-10.6685608540561,-10.1836262697808,-10.1391126103836),
 .UNSPECIFIED.);
#679=B_SPLINE_CURVE_WITH_KNOTS('',3,(#33234,#33235,#33236,#33237,#33238,
#33239,#33240,#33241,#33242,#33243,#33244,#33245,#33246,#33247,#33248,#33249,
#33250,#33251,#33252,#33253,#33254,#33255,#33256,#33257,#33258),
 .UNSPECIFIED.,.F.,.F.,(4,3,3,3,3,3,3,3,4),(-3.85592730320397,-3.39454208992695,
-2.90960750565167,-2.42467292137639,-1.93973833710111,-1.45480375282583,
-0.969869168550554,-0.484934584275278,0.),.UNSPECIFIED.);
#680=B_SPLINE_CURVE_WITH_KNOTS('',3,(#33261,#33262,#33263,#33264,#33265,
#33266,#33267,#33268,#33269,#33270,#33271,#33272,#33273,#33274,#33275,#33276,
#33277,#33278,#33279,#33280,#33281,#33282,#33283,#33284,#33285,#33286,#33287,
#33288,#33289,#33290,#33291,#33292,#33293,#33294,#33295,#33296,#33297),
 .UNSPECIFIED.,.F.,.F.,(4,3,3,3,3,3,3,3,3,3,3,3,4),(2.02359549069725,2.42467292137639,
2.90960750565167,3.39454208992695,3.87947667420223,4.36441125847751,4.84934584275279,
5.33428042702807,5.81921501130334,6.30414959557862,6.7890841798539,7.27401876412918,
7.59244614826264),.UNSPECIFIED.);
#681=B_SPLINE_CURVE_WITH_KNOTS('',3,(#33303,#33304,#33305,#33306,#33307,
#33308,#33309,#33310,#33311,#33312,#33313,#33314,#33315),.UNSPECIFIED.,
 .F.,.F.,(4,1,1,1,1,1,1,1,1,1,4),(34.5575191894877,34.6439614256831,35.1288960099583,
35.6138305942336,36.0987651785089,36.5836997627842,37.0686343470595,37.5535689313347,
38.03850351561,38.5234380998853,39.0083726841606),.UNSPECIFIED.);
#682=B_SPLINE_CURVE_WITH_KNOTS('',3,(#33318,#33319,#33320,#33321,#33322,
#33323,#33324,#33325,#33326,#33327,#33328,#33329,#33330,#33331),
 .UNSPECIFIED.,.F.,.F.,(4,1,1,1,1,1,1,1,1,1,1,4),(34.5575191894877,34.7659549664276,
35.2508895507029,35.7358241349782,36.2207587192535,36.7056933035287,37.190627887804,
37.6755624720793,38.1604970563546,38.6454316406298,39.1303662249051,39.5314436555842),
 .UNSPECIFIED.);
#683=B_SPLINE_CURVE_WITH_KNOTS('',3,(#33336,#33337,#33338,#33339,#33340,
#33341,#33342,#33343,#33344,#33345,#33346,#33347,#33348,#33349,#33350,#33351,
#33352),.UNSPECIFIED.,.F.,.F.,(4,1,1,1,1,1,1,1,1,1,1,1,1,1,4),(28.2743338823082,
28.3398118301045,28.8247464143797,29.309680998655,29.7946155829303,30.2795501672056,
30.7644847514808,31.2494193357561,31.7343539200314,32.2192885043067,32.704223088582,
33.1891576728572,33.6740922571325,34.1590268414078,34.5575191894877),
 .UNSPECIFIED.);
#684=B_SPLINE_CURVE_WITH_KNOTS('',3,(#33353,#33354,#33355,#33356,#33357,
#33358,#33359,#33360,#33361,#33362,#33363,#33364,#33365,#33366,#33367,#33368,
#33369),.UNSPECIFIED.,.F.,.F.,(4,1,1,1,1,1,1,1,1,1,1,1,1,1,4),(28.2743338823082,
28.461805370849,28.9467399551243,29.4316745393995,29.9166091236748,30.4015437079501,
30.8864782922254,31.3714128765007,31.8563474607759,32.3412820450512,32.8262166293265,
33.3111512136018,33.7960857978771,34.2810203821523,34.5575191894877),
 .UNSPECIFIED.);
#685=B_SPLINE_CURVE_WITH_KNOTS('',3,(#33374,#33375,#33376,#33377,#33378,
#33379,#33380,#33381,#33382,#33383,#33384,#33385,#33386,#33387,#33388,#33389,
#33390),.UNSPECIFIED.,.F.,.F.,(4,1,1,1,1,1,1,1,1,1,1,1,1,1,4),(21.9911485751286,
22.0356622345258,22.5205968188011,23.0055314030764,23.4904659873517,23.9754005716269,
24.4603351559022,24.9452697401775,25.4302043244528,25.9151389087281,26.4000734930033,
26.8850080772786,27.3699426615539,27.8548772458292,28.2743338823082),
 .UNSPECIFIED.);
#686=B_SPLINE_CURVE_WITH_KNOTS('',3,(#33391,#33392,#33393,#33394,#33395,
#33396,#33397,#33398,#33399,#33400,#33401,#33402,#33403,#33404,#33405,#33406,
#33407),.UNSPECIFIED.,.F.,.F.,(4,1,1,1,1,1,1,1,1,1,1,1,1,1,4),(21.9911485751286,
22.1576557752704,22.6425903595456,23.1275249438209,23.6124595280962,24.0973941123715,
24.5823286966468,25.067263280922,25.5521978651973,26.0371324494726,26.5220670337479,
27.0070016180232,27.4919362022984,27.9768707865737,28.2743338823082),
 .UNSPECIFIED.);
#687=B_SPLINE_CURVE_WITH_KNOTS('',3,(#33413,#33414,#33415,#33416,#33417,
#33418),.UNSPECIFIED.,.F.,.F.,(4,1,1,4),(14.3987024268659,14.8836370111412,
15.3685715954165,15.707963267949),.UNSPECIFIED.);
#688=B_SPLINE_CURVE_WITH_KNOTS('',3,(#33421,#33422,#33423,#33424,#33425,
#33426,#33427),.UNSPECIFIED.,.F.,.F.,(4,1,1,1,4),(13.8756314554422,14.2767088861214,
14.7616434703967,15.2465780546719,15.707963267949),.UNSPECIFIED.);
#689=B_SPLINE_CURVE_WITH_KNOTS('',3,(#33429,#33430,#33431,#33432,#33433,
#33434,#33435,#33436,#33437,#33438,#33439,#33440,#33441,#33442,#33443,#33444,
#33445),.UNSPECIFIED.,.F.,.F.,(4,1,1,1,1,1,1,1,1,1,1,1,1,1,4),(15.707963267949,
15.7315126389472,16.2164472232225,16.7013818074978,17.1863163917731,17.6712509760483,
18.1561855603236,18.6411201445989,19.1260547288742,19.6109893131494,20.0959238974247,
20.5808584817,21.0657930659753,21.5507276502506,21.9911485751286),
 .UNSPECIFIED.);
#690=B_SPLINE_CURVE_WITH_KNOTS('',3,(#33446,#33447,#33448,#33449,#33450,
#33451,#33452,#33453,#33454,#33455,#33456,#33457,#33458,#33459,#33460,#33461,
#33462),.UNSPECIFIED.,.F.,.F.,(4,1,1,1,1,1,1,1,1,1,1,1,1,1,4),(15.707963267949,
15.8535061796917,16.338440763967,16.8233753482423,17.3083099325176,17.7932445167929,
18.2781791010681,18.7631136853434,19.2480482696187,19.732982853894,20.2179174381693,
20.7028520224445,21.1877866067198,21.6727211909951,21.9911485751286),
 .UNSPECIFIED.);
#691=B_SPLINE_CURVE_WITH_KNOTS('',3,(#33699,#33700,#33701,#33702,#33703,
#33704,#33705,#33706,#33707,#33708,#33709,#33710,#33711,#33712,#33713,#33714,
#33715,#33716,#33717,#33718,#33719,#33720,#33721,#33722,#33723,#33724,#33725,
#33726,#33727,#33728,#33729,#33730,#33731,#33732,#33733,#33734,#33735,#33736,
#33737,#33738,#33739,#33740,#33741,#33742,#33743,#33744,#33745,#33746,#33747,
#33748,#33749,#33750,#33751,#33752,#33753,#33754,#33755,#33756,#33757,#33758,
#33759,#33760,#33761,#33762,#33763,#33764,#33765,#33766,#33767,#33768,#33769,
#33770,#33771,#33772,#33773,#33774,#33775,#33776,#33777),.UNSPECIFIED.,
 .F.,.F.,(4,3,3,3,3,3,3,3,3,3,3,3,3,3,3,3,3,3,3,3,3,3,3,3,3,3,4),(0.,0.152215598280746,
0.304359127092899,0.444170208698824,0.47198649256547,0.58398129030475,0.733405388599423,
0.837349658265653,0.892797098974412,0.921010909097056,0.951233547269046,
1.0971204053036,1.14918246726435,1.28571136325164,1.34308246486694,1.37129903143152,
1.514527111463,1.65613233320033,1.69529805121353,1.76334988113777,1.79789380048528,
1.82919292778863,1.96987782168459,2.04822510610851,2.08147567267347,2.22116640322417,
2.31010750305849),.UNSPECIFIED.);
#692=B_SPLINE_CURVE_WITH_KNOTS('',3,(#33778,#33779,#33780,#33781,#33782,
#33783,#33784,#33785,#33786,#33787,#33788,#33789,#33790,#33791,#33792,#33793,
#33794,#33795,#33796,#33797,#33798,#33799,#33800,#33801,#33802,#33803,#33804,
#33805,#33806,#33807,#33808,#33809,#33810,#33811,#33812,#33813,#33814,#33815,
#33816,#33817,#33818,#33819,#33820,#33821,#33822,#33823,#33824,#33825,#33826,
#33827,#33828,#33829,#33830,#33831,#33832,#33833,#33834,#33835,#33836,#33837,
#33838,#33839,#33840,#33841,#33842,#33843,#33844,#33845,#33846,#33847,#33848,
#33849,#33850,#33851,#33852,#33853),.UNSPECIFIED.,.F.,.F.,(4,3,3,3,3,3,
3,3,3,3,3,3,3,3,3,3,3,3,3,3,3,3,3,3,3,4),(0.,0.136942003107033,0.275838247773224,
0.398831227256207,0.433644454679001,0.521824206739189,0.663226927758571,
0.763151769253735,0.825069330101608,0.861088517754105,1.00600779023923,
1.06292629373923,1.20295657612769,1.26303420725827,1.30095884831302,1.44786364908515,
1.59610962438193,1.62304742329308,1.69648826922106,1.73120226201003,1.76336667156587,
1.91360294366234,1.99760348846723,2.041326271508,2.20106314648742,2.30292298333822),
 .UNSPECIFIED.);
#693=B_SPLINE_CURVE_WITH_KNOTS('',3,(#33854,#33855,#33856,#33857,#33858,
#33859,#33860,#33861,#33862,#33863,#33864,#33865,#33866,#33867,#33868,#33869,
#33870,#33871,#33872,#33873,#33874,#33875,#33876,#33877,#33878,#33879,#33880,
#33881,#33882,#33883,#33884,#33885,#33886,#33887,#33888,#33889,#33890,#33891,
#33892,#33893,#33894,#33895,#33896),.UNSPECIFIED.,.F.,.F.,(4,3,3,3,3,3,
3,3,3,3,3,3,3,3,4),(-10.1391126103836,-9.69869168550557,-9.21375710123029,
-8.72882251695501,-8.24388793267973,-7.75895334840445,-7.27401876412917,
-6.7890841798539,-6.30414959557862,-5.81921501130334,-5.33428042702806,
-4.84934584275278,-4.3644112584775,-3.87947667420223,-3.85592730320397),
 .UNSPECIFIED.);
#694=B_SPLINE_CURVE_WITH_KNOTS('',3,(#34133,#34134,#34135,#34136,#34137,
#34138,#34139,#34140,#34141,#34142,#34143,#34144,#34145,#34146,#34147,#34148,
#34149,#34150,#34151,#34152,#34153,#34154,#34155,#34156,#34157,#34158,#34159,
#34160,#34161,#34162,#34163,#34164,#34165,#34166,#34167,#34168,#34169,#34170,
#34171,#34172,#34173,#34174,#34175,#34176,#34177,#34178,#34179,#34180,#34181,
#34182,#34183,#34184,#34185,#34186,#34187,#34188,#34189,#34190,#34191,#34192,
#34193,#34194,#34195,#34196,#34197,#34198,#34199,#34200,#34201,#34202,#34203,
#34204,#34205,#34206,#34207,#34208),.UNSPECIFIED.,.F.,.F.,(4,3,3,3,3,3,
3,3,3,3,3,3,3,3,3,3,3,3,3,3,3,3,3,3,3,4),(0.,0.136941909255917,0.275838110703575,
0.39883115872138,0.433644442051902,0.521824206739185,0.663226972733855,
0.763151802985195,0.825069431517984,0.861088523135606,1.00600782795853,
1.06292629373921,1.20295657612768,1.26303420748856,1.30095884865492,1.44786363673769,
1.59610960975183,1.62304742329307,1.69648826990486,1.73120226945793,1.76336667330399,
1.91360294448452,1.99760349002108,2.04132627244116,2.20106314648741,2.30292298333825),
 .UNSPECIFIED.);
#695=B_SPLINE_CURVE_WITH_KNOTS('',3,(#34209,#34210,#34211,#34212,#34213,
#34214,#34215,#34216,#34217,#34218,#34219,#34220,#34221,#34222,#34223,#34224,
#34225,#34226,#34227,#34228,#34229,#34230,#34231,#34232,#34233,#34234,#34235,
#34236,#34237,#34238,#34239,#34240,#34241,#34242,#34243,#34244,#34245,#34246,
#34247,#34248,#34249,#34250,#34251),.UNSPECIFIED.,.F.,.F.,(4,3,3,3,3,3,
3,3,3,3,3,3,3,3,4),(7.59244614826264,7.75895334840446,8.24388793267974,
8.72882251695502,9.2137571012303,9.69869168550558,10.1836262697809,10.6685608540561,
11.1534954383314,11.6384300226067,12.123364606882,12.6082991911572,13.0932337754325,
13.5781683597078,13.8756314554422),.UNSPECIFIED.);
#696=B_SPLINE_CURVE_WITH_KNOTS('',3,(#34252,#34253,#34254,#34255,#34256,
#34257,#34258,#34259,#34260,#34261,#34262,#34263,#34264,#34265,#34266,#34267,
#34268,#34269,#34270,#34271,#34272,#34273,#34274,#34275,#34276,#34277,#34278,
#34279,#34280,#34281,#34282,#34283,#34284,#34285,#34286,#34287,#34288,#34289,
#34290,#34291,#34292,#34293,#34294,#34295,#34296,#34297,#34298,#34299,#34300,
#34301,#34302,#34303,#34304,#34305,#34306,#34307,#34308,#34309,#34310,#34311,
#34312,#34313,#34314,#34315,#34316,#34317,#34318,#34319,#34320,#34321,#34322,
#34323,#34324,#34325,#34326,#34327,#34328,#34329,#34330),.UNSPECIFIED.,
 .F.,.F.,(4,3,3,3,3,3,3,3,3,3,3,3,3,3,3,3,3,3,3,3,3,3,3,3,3,3,4),(0.,0.152215561651553,
0.304359114914711,0.444170202609736,0.471986489091098,0.583981290304761,
0.733405394542357,0.837349662722867,0.892797117478666,0.921010855072337,
0.951233541121055,1.09712039568669,1.1491824672644,1.28571136325172,1.34308246731324,
1.37129903319467,1.51452711094878,1.65613232955333,1.69529805121367,1.76334988194098,
1.79789380901942,1.82919292981007,1.96987782454073,2.04822511067641,2.0814756771912,
2.22116640322435,2.31010750305867),.UNSPECIFIED.);
#718=SHAPE_REPRESENTATION_RELATIONSHIP('SRR','None',#34564,#740);
#740=ADVANCED_BREP_SHAPE_REPRESENTATION('',(#798),#34432);
#770=STYLED_ITEM('',(#34750),#798);
#798=MANIFOLD_SOLID_BREP('Body1',#8799);
#855=FACE_BOUND('',#2066,.T.);
#856=FACE_BOUND('',#2075,.T.);
#1036=PLANE('',#9710);
#1037=PLANE('',#9712);
#1038=PLANE('',#9713);
#1039=PLANE('',#9714);
#1040=PLANE('',#9715);
#1041=PLANE('',#9716);
#1042=PLANE('',#9717);
#1043=PLANE('',#9718);
#1511=FACE_OUTER_BOUND('',#2054,.T.);
#1512=FACE_OUTER_BOUND('',#2055,.T.);
#1513=FACE_OUTER_BOUND('',#2056,.T.);
#1514=FACE_OUTER_BOUND('',#2057,.T.);
#1515=FACE_OUTER_BOUND('',#2058,.T.);
#1516=FACE_OUTER_BOUND('',#2059,.T.);
#1517=FACE_OUTER_BOUND('',#2060,.T.);
#1518=FACE_OUTER_BOUND('',#2061,.T.);
#1519=FACE_OUTER_BOUND('',#2062,.T.);
#1520=FACE_OUTER_BOUND('',#2063,.T.);
#1521=FACE_OUTER_BOUND('',#2064,.T.);
#1522=FACE_OUTER_BOUND('',#2065,.T.);
#1523=FACE_OUTER_BOUND('',#2067,.T.);
#1524=FACE_OUTER_BOUND('',#2068,.T.);
#1525=FACE_OUTER_BOUND('',#2069,.T.);
#1526=FACE_OUTER_BOUND('',#2070,.T.);
#1527=FACE_OUTER_BOUND('',#2071,.T.);
#1528=FACE_OUTER_BOUND('',#2072,.T.);
#1529=FACE_OUTER_BOUND('',#2073,.T.);
#1530=FACE_OUTER_BOUND('',#2074,.T.);
#2054=EDGE_LOOP('',(#7891,#7892,#7893,#7894));
#2055=EDGE_LOOP('',(#7895,#7896,#7897,#7898));
#2056=EDGE_LOOP('',(#7899,#7900,#7901,#7902));
#2057=EDGE_LOOP('',(#7903,#7904,#7905,#7906));
#2058=EDGE_LOOP('',(#7907,#7908,#7909,#7910));
#2059=EDGE_LOOP('',(#7911,#7912,#7913,#7914));
#2060=EDGE_LOOP('',(#7915,#7916,#7917,#7918));
#2061=EDGE_LOOP('',(#7919,#7920,#7921,#7922));
#2062=EDGE_LOOP('',(#7923,#7924,#7925,#7926));
#2063=EDGE_LOOP('',(#7927,#7928,#7929,#7930,#7931,#7932,#7933,#7934,#7935,
#7936,#7937,#7938));
#2064=EDGE_LOOP('',(#7939,#7940,#7941,#7942,#7943,#7944,#7945,#7946,#7947,
#7948,#7949,#7950));
#2065=EDGE_LOOP('',(#7951,#7952,#7953,#7954,#7955,#7956));
#2066=EDGE_LOOP('',(#7957,#7958,#7959,#7960));
#2067=EDGE_LOOP('',(#7961,#7962,#7963,#7964));
#2068=EDGE_LOOP('',(#7965,#7966,#7967,#7968));
#2069=EDGE_LOOP('',(#7969,#7970,#7971,#7972));
#2070=EDGE_LOOP('',(#7973,#7974,#7975,#7976));
#2071=EDGE_LOOP('',(#7977,#7978,#7979,#7980));
#2072=EDGE_LOOP('',(#7981,#7982,#7983,#7984));
#2073=EDGE_LOOP('',(#7985,#7986,#7987,#7988));
#2074=EDGE_LOOP('',(#7989,#7990,#7991,#7992,#7993,#7994));
#2075=EDGE_LOOP('',(#7995,#7996,#7997,#7998));
#2667=LINE('',#33019,#3284);
#2668=LINE('',#33052,#3285);
#2669=LINE('',#33142,#3286);
#2670=LINE('',#33232,#3287);
#2671=LINE('',#33301,#3288);
#2672=LINE('',#33335,#3289);
#2673=LINE('',#33373,#3290);
#2674=LINE('',#33411,#3291);
#2675=LINE('',#34334,#3292);
#2676=LINE('',#34336,#3293);
#2677=LINE('',#34338,#3294);
#2678=LINE('',#34340,#3295);
#2679=LINE('',#34342,#3296);
#2680=LINE('',#34343,#3297);
#2681=LINE('',#34348,#3298);
#2682=LINE('',#34349,#3299);
#2683=LINE('',#34350,#3300);
#2684=LINE('',#34353,#3301);
#2685=LINE('',#34354,#3302);
#2686=LINE('',#34357,#3303);
#2687=LINE('',#34358,#3304);
#2688=LINE('',#34361,#3305);
#2689=LINE('',#34362,#3306);
#2690=LINE('',#34365,#3307);
#2691=LINE('',#34366,#3308);
#2692=LINE('',#34368,#3309);
#3284=VECTOR('',#11626,1.05);
#3285=VECTOR('',#11631,1.05);
#3286=VECTOR('',#11634,1.05);
#3287=VECTOR('',#11637,1.05);
#3288=VECTOR('',#11642,1.21745);
#3289=VECTOR('',#11647,1.21745);
#3290=VECTOR('',#11650,1.21745);
#3291=VECTOR('',#11653,1.21745);
#3292=VECTOR('',#11660,1.);
#3293=VECTOR('',#11661,1.);
#3294=VECTOR('',#11662,1.);
#3295=VECTOR('',#11663,1.);
#3296=VECTOR('',#11664,1.);
#3297=VECTOR('',#11665,1.);
#3298=VECTOR('',#11670,1.);
#3299=VECTOR('',#11671,1.);
#3300=VECTOR('',#11672,1.);
#3301=VECTOR('',#11675,1.);
#3302=VECTOR('',#11676,1.);
#3303=VECTOR('',#11679,1.);
#3304=VECTOR('',#11680,1.);
#3305=VECTOR('',#11683,1.);
#3306=VECTOR('',#11684,1.);
#3307=VECTOR('',#11687,1.);
#3308=VECTOR('',#11688,1.);
#3309=VECTOR('',#11691,1.);
#3440=CIRCLE('',#9698,1.0501);
#3441=CIRCLE('',#9702,1.0501);
#3442=CIRCLE('',#9704,1.21745);
#3443=CIRCLE('',#9708,1.21745);
#4234=VERTEX_POINT('',#33017);
#4235=VERTEX_POINT('',#33018);
#4236=VERTEX_POINT('',#33020);
#4237=VERTEX_POINT('',#33028);
#4238=VERTEX_POINT('',#33050);
#4239=VERTEX_POINT('',#33051);
#4240=VERTEX_POINT('',#33140);
#4241=VERTEX_POINT('',#33141);
#4242=VERTEX_POINT('',#33230);
#4243=VERTEX_POINT('',#33231);
#4244=VERTEX_POINT('',#33233);
#4245=VERTEX_POINT('',#33259);
#4246=VERTEX_POINT('',#33299);
#4247=VERTEX_POINT('',#33300);
#4248=VERTEX_POINT('',#33302);
#4249=VERTEX_POINT('',#33316);
#4250=VERTEX_POINT('',#33333);
#4251=VERTEX_POINT('',#33334);
#4252=VERTEX_POINT('',#33371);
#4253=VERTEX_POINT('',#33372);
#4254=VERTEX_POINT('',#33409);
#4255=VERTEX_POINT('',#33410);
#4256=VERTEX_POINT('',#33412);
#4257=VERTEX_POINT('',#33419);
#4258=VERTEX_POINT('',#34332);
#4259=VERTEX_POINT('',#34333);
#4260=VERTEX_POINT('',#34335);
#4261=VERTEX_POINT('',#34337);
#4262=VERTEX_POINT('',#34339);
#4263=VERTEX_POINT('',#34341);
#4264=VERTEX_POINT('',#34346);
#4265=VERTEX_POINT('',#34347);
#4266=VERTEX_POINT('',#34352);
#4267=VERTEX_POINT('',#34356);
#4268=VERTEX_POINT('',#34360);
#4269=VERTEX_POINT('',#34364);
#5459=EDGE_CURVE('',#4234,#4235,#2667,.T.);
#5460=EDGE_CURVE('',#4235,#4236,#673,.T.);
#5461=EDGE_CURVE('',#4237,#4236,#3440,.T.);
#5462=EDGE_CURVE('',#4237,#4234,#674,.T.);
#5463=EDGE_CURVE('',#4238,#4239,#2668,.T.);
#5464=EDGE_CURVE('',#4239,#4235,#675,.T.);
#5465=EDGE_CURVE('',#4234,#4238,#676,.T.);
#5466=EDGE_CURVE('',#4240,#4241,#2669,.T.);
#5467=EDGE_CURVE('',#4241,#4239,#677,.T.);
#5468=EDGE_CURVE('',#4238,#4240,#678,.T.);
#5469=EDGE_CURVE('',#4242,#4243,#2670,.T.);
#5470=EDGE_CURVE('',#4242,#4244,#679,.T.);
#5471=EDGE_CURVE('',#4245,#4244,#3441,.F.);
#5472=EDGE_CURVE('',#4245,#4243,#680,.T.);
#5473=EDGE_CURVE('',#4246,#4247,#2671,.T.);
#5474=EDGE_CURVE('',#4247,#4248,#681,.T.);
#5475=EDGE_CURVE('',#4249,#4248,#3442,.T.);
#5476=EDGE_CURVE('',#4246,#4249,#682,.T.);
#5477=EDGE_CURVE('',#4250,#4251,#2672,.T.);
#5478=EDGE_CURVE('',#4251,#4247,#683,.T.);
#5479=EDGE_CURVE('',#4250,#4246,#684,.T.);
#5480=EDGE_CURVE('',#4252,#4253,#2673,.T.);
#5481=EDGE_CURVE('',#4253,#4251,#685,.T.);
#5482=EDGE_CURVE('',#4252,#4250,#686,.T.);
#5483=EDGE_CURVE('',#4254,#4255,#2674,.T.);
#5484=EDGE_CURVE('',#4256,#4254,#687,.T.);
#5485=EDGE_CURVE('',#4257,#4256,#3443,.T.);
#5486=EDGE_CURVE('',#4257,#4255,#688,.T.);
#5487=EDGE_CURVE('',#4255,#4253,#689,.T.);
#5488=EDGE_CURVE('',#4254,#4252,#690,.T.);
#5489=EDGE_CURVE('',#4248,#4237,#691,.T.);
#5490=EDGE_CURVE('',#4244,#4257,#692,.T.);
#5491=EDGE_CURVE('',#4240,#4242,#693,.T.);
#5492=EDGE_CURVE('',#4236,#4249,#694,.T.);
#5493=EDGE_CURVE('',#4243,#4241,#695,.T.);
#5494=EDGE_CURVE('',#4256,#4245,#696,.T.);
#5495=EDGE_CURVE('',#4258,#4259,#2675,.T.);
#5496=EDGE_CURVE('',#4259,#4260,#2676,.T.);
#5497=EDGE_CURVE('',#4260,#4261,#2677,.T.);
#5498=EDGE_CURVE('',#4261,#4262,#2678,.T.);
#5499=EDGE_CURVE('',#4262,#4263,#2679,.T.);
#5500=EDGE_CURVE('',#4263,#4258,#2680,.T.);
#5501=EDGE_CURVE('',#4264,#4265,#2681,.T.);
#5502=EDGE_CURVE('',#4265,#4258,#2682,.T.);
#5503=EDGE_CURVE('',#4264,#4263,#2683,.T.);
#5504=EDGE_CURVE('',#4266,#4264,#2684,.T.);
#5505=EDGE_CURVE('',#4266,#4262,#2685,.T.);
#5506=EDGE_CURVE('',#4267,#4266,#2686,.T.);
#5507=EDGE_CURVE('',#4267,#4261,#2687,.T.);
#5508=EDGE_CURVE('',#4268,#4267,#2688,.T.);
#5509=EDGE_CURVE('',#4268,#4260,#2689,.T.);
#5510=EDGE_CURVE('',#4269,#4268,#2690,.T.);
#5511=EDGE_CURVE('',#4269,#4259,#2691,.T.);
#5512=EDGE_CURVE('',#4265,#4269,#2692,.T.);
#7891=ORIENTED_EDGE('',*,*,#5459,.T.);
#7892=ORIENTED_EDGE('',*,*,#5460,.T.);
#7893=ORIENTED_EDGE('',*,*,#5461,.F.);
#7894=ORIENTED_EDGE('',*,*,#5462,.T.);
#7895=ORIENTED_EDGE('',*,*,#5463,.T.);
#7896=ORIENTED_EDGE('',*,*,#5464,.T.);
#7897=ORIENTED_EDGE('',*,*,#5459,.F.);
#7898=ORIENTED_EDGE('',*,*,#5465,.T.);
#7899=ORIENTED_EDGE('',*,*,#5466,.T.);
#7900=ORIENTED_EDGE('',*,*,#5467,.T.);
#7901=ORIENTED_EDGE('',*,*,#5463,.F.);
#7902=ORIENTED_EDGE('',*,*,#5468,.T.);
#7903=ORIENTED_EDGE('',*,*,#5469,.F.);
#7904=ORIENTED_EDGE('',*,*,#5470,.T.);
#7905=ORIENTED_EDGE('',*,*,#5471,.F.);
#7906=ORIENTED_EDGE('',*,*,#5472,.T.);
#7907=ORIENTED_EDGE('',*,*,#5473,.T.);
#7908=ORIENTED_EDGE('',*,*,#5474,.T.);
#7909=ORIENTED_EDGE('',*,*,#5475,.F.);
#7910=ORIENTED_EDGE('',*,*,#5476,.F.);
#7911=ORIENTED_EDGE('',*,*,#5477,.T.);
#7912=ORIENTED_EDGE('',*,*,#5478,.T.);
#7913=ORIENTED_EDGE('',*,*,#5473,.F.);
#7914=ORIENTED_EDGE('',*,*,#5479,.F.);
#7915=ORIENTED_EDGE('',*,*,#5480,.T.);
#7916=ORIENTED_EDGE('',*,*,#5481,.T.);
#7917=ORIENTED_EDGE('',*,*,#5477,.F.);
#7918=ORIENTED_EDGE('',*,*,#5482,.F.);
#7919=ORIENTED_EDGE('',*,*,#5483,.F.);
#7920=ORIENTED_EDGE('',*,*,#5484,.F.);
#7921=ORIENTED_EDGE('',*,*,#5485,.F.);
#7922=ORIENTED_EDGE('',*,*,#5486,.T.);
#7923=ORIENTED_EDGE('',*,*,#5483,.T.);
#7924=ORIENTED_EDGE('',*,*,#5487,.T.);
#7925=ORIENTED_EDGE('',*,*,#5480,.F.);
#7926=ORIENTED_EDGE('',*,*,#5488,.F.);
#7927=ORIENTED_EDGE('',*,*,#5489,.F.);
#7928=ORIENTED_EDGE('',*,*,#5474,.F.);
#7929=ORIENTED_EDGE('',*,*,#5478,.F.);
#7930=ORIENTED_EDGE('',*,*,#5481,.F.);
#7931=ORIENTED_EDGE('',*,*,#5487,.F.);
#7932=ORIENTED_EDGE('',*,*,#5486,.F.);
#7933=ORIENTED_EDGE('',*,*,#5490,.F.);
#7934=ORIENTED_EDGE('',*,*,#5470,.F.);
#7935=ORIENTED_EDGE('',*,*,#5491,.F.);
#7936=ORIENTED_EDGE('',*,*,#5468,.F.);
#7937=ORIENTED_EDGE('',*,*,#5465,.F.);
#7938=ORIENTED_EDGE('',*,*,#5462,.F.);
#7939=ORIENTED_EDGE('',*,*,#5492,.F.);
#7940=ORIENTED_EDGE('',*,*,#5460,.F.);
#7941=ORIENTED_EDGE('',*,*,#5464,.F.);
#7942=ORIENTED_EDGE('',*,*,#5467,.F.);
#7943=ORIENTED_EDGE('',*,*,#5493,.F.);
#7944=ORIENTED_EDGE('',*,*,#5472,.F.);
#7945=ORIENTED_EDGE('',*,*,#5494,.F.);
#7946=ORIENTED_EDGE('',*,*,#5484,.T.);
#7947=ORIENTED_EDGE('',*,*,#5488,.T.);
#7948=ORIENTED_EDGE('',*,*,#5482,.T.);
#7949=ORIENTED_EDGE('',*,*,#5479,.T.);
#7950=ORIENTED_EDGE('',*,*,#5476,.T.);
#7951=ORIENTED_EDGE('',*,*,#5495,.T.);
#7952=ORIENTED_EDGE('',*,*,#5496,.T.);
#7953=ORIENTED_EDGE('',*,*,#5497,.T.);
#7954=ORIENTED_EDGE('',*,*,#5498,.T.);
#7955=ORIENTED_EDGE('',*,*,#5499,.T.);
#7956=ORIENTED_EDGE('',*,*,#5500,.T.);
#7957=ORIENTED_EDGE('',*,*,#5492,.T.);
#7958=ORIENTED_EDGE('',*,*,#5475,.T.);
#7959=ORIENTED_EDGE('',*,*,#5489,.T.);
#7960=ORIENTED_EDGE('',*,*,#5461,.T.);
#7961=ORIENTED_EDGE('',*,*,#5469,.T.);
#7962=ORIENTED_EDGE('',*,*,#5493,.T.);
#7963=ORIENTED_EDGE('',*,*,#5466,.F.);
#7964=ORIENTED_EDGE('',*,*,#5491,.T.);
#7965=ORIENTED_EDGE('',*,*,#5501,.T.);
#7966=ORIENTED_EDGE('',*,*,#5502,.T.);
#7967=ORIENTED_EDGE('',*,*,#5500,.F.);
#7968=ORIENTED_EDGE('',*,*,#5503,.F.);
#7969=ORIENTED_EDGE('',*,*,#5504,.T.);
#7970=ORIENTED_EDGE('',*,*,#5503,.T.);
#7971=ORIENTED_EDGE('',*,*,#5499,.F.);
#7972=ORIENTED_EDGE('',*,*,#5505,.F.);
#7973=ORIENTED_EDGE('',*,*,#5506,.T.);
#7974=ORIENTED_EDGE('',*,*,#5505,.T.);
#7975=ORIENTED_EDGE('',*,*,#5498,.F.);
#7976=ORIENTED_EDGE('',*,*,#5507,.F.);
#7977=ORIENTED_EDGE('',*,*,#5508,.T.);
#7978=ORIENTED_EDGE('',*,*,#5507,.T.);
#7979=ORIENTED_EDGE('',*,*,#5497,.F.);
#7980=ORIENTED_EDGE('',*,*,#5509,.F.);
#7981=ORIENTED_EDGE('',*,*,#5510,.T.);
#7982=ORIENTED_EDGE('',*,*,#5509,.T.);
#7983=ORIENTED_EDGE('',*,*,#5496,.F.);
#7984=ORIENTED_EDGE('',*,*,#5511,.F.);
#7985=ORIENTED_EDGE('',*,*,#5512,.T.);
#7986=ORIENTED_EDGE('',*,*,#5511,.T.);
#7987=ORIENTED_EDGE('',*,*,#5495,.F.);
#7988=ORIENTED_EDGE('',*,*,#5502,.F.);
#7989=ORIENTED_EDGE('',*,*,#5512,.F.);
#7990=ORIENTED_EDGE('',*,*,#5501,.F.);
#7991=ORIENTED_EDGE('',*,*,#5504,.F.);
#7992=ORIENTED_EDGE('',*,*,#5506,.F.);
#7993=ORIENTED_EDGE('',*,*,#5508,.F.);
#7994=ORIENTED_EDGE('',*,*,#5510,.F.);
#7995=ORIENTED_EDGE('',*,*,#5494,.T.);
#7996=ORIENTED_EDGE('',*,*,#5471,.T.);
#7997=ORIENTED_EDGE('',*,*,#5490,.T.);
#7998=ORIENTED_EDGE('',*,*,#5485,.T.);
#8271=CYLINDRICAL_SURFACE('',#9697,1.0501);
#8272=CYLINDRICAL_SURFACE('',#9699,1.0501);
#8273=CYLINDRICAL_SURFACE('',#9700,1.0501);
#8274=CYLINDRICAL_SURFACE('',#9701,1.0501);
#8275=CYLINDRICAL_SURFACE('',#9703,1.21745);
#8276=CYLINDRICAL_SURFACE('',#9705,1.21745);
#8277=CYLINDRICAL_SURFACE('',#9706,1.21745);
#8278=CYLINDRICAL_SURFACE('',#9707,1.21745);
#8279=CYLINDRICAL_SURFACE('',#9709,1.21745);
#8280=CYLINDRICAL_SURFACE('',#9711,1.0501);
#8748=ADVANCED_FACE('',(#1511),#8271,.F.);
#8749=ADVANCED_FACE('',(#1512),#8272,.F.);
#8750=ADVANCED_FACE('',(#1513),#8273,.F.);
#8751=ADVANCED_FACE('',(#1514),#8274,.F.);
#8752=ADVANCED_FACE('',(#1515),#8275,.F.);
#8753=ADVANCED_FACE('',(#1516),#8276,.F.);
#8754=ADVANCED_FACE('',(#1517),#8277,.F.);
#8755=ADVANCED_FACE('',(#1518),#8278,.F.);
#8756=ADVANCED_FACE('',(#1519),#8279,.F.);
#8757=ADVANCED_FACE('',(#1520),#215,.F.);
#8758=ADVANCED_FACE('',(#1521),#216,.F.);
#8759=ADVANCED_FACE('',(#1522,#855),#1036,.T.);
#8760=ADVANCED_FACE('',(#1523),#8280,.F.);
#8761=ADVANCED_FACE('',(#1524),#1037,.T.);
#8762=ADVANCED_FACE('',(#1525),#1038,.T.);
#8763=ADVANCED_FACE('',(#1526),#1039,.T.);
#8764=ADVANCED_FACE('',(#1527),#1040,.T.);
#8765=ADVANCED_FACE('',(#1528),#1041,.T.);
#8766=ADVANCED_FACE('',(#1529),#1042,.T.);
#8767=ADVANCED_FACE('',(#1530,#856),#1043,.F.);
#8799=CLOSED_SHELL('',(#8748,#8749,#8750,#8751,#8752,#8753,#8754,#8755,
#8756,#8757,#8758,#8759,#8760,#8761,#8762,#8763,#8764,#8765,#8766,#8767));
#9696=AXIS2_PLACEMENT_3D('',#33015,#11622,#11623);
#9697=AXIS2_PLACEMENT_3D('',#33016,#11624,#11625);
#9698=AXIS2_PLACEMENT_3D('',#33029,#11627,#11628);
#9699=AXIS2_PLACEMENT_3D('',#33049,#11629,#11630);
#9700=AXIS2_PLACEMENT_3D('',#33139,#11632,#11633);
#9701=AXIS2_PLACEMENT_3D('',#33229,#11635,#11636);
#9702=AXIS2_PLACEMENT_3D('',#33260,#11638,#11639);
#9703=AXIS2_PLACEMENT_3D('',#33298,#11640,#11641);
#9704=AXIS2_PLACEMENT_3D('',#33317,#11643,#11644);
#9705=AXIS2_PLACEMENT_3D('',#33332,#11645,#11646);
#9706=AXIS2_PLACEMENT_3D('',#33370,#11648,#11649);
#9707=AXIS2_PLACEMENT_3D('',#33408,#11651,#11652);
#9708=AXIS2_PLACEMENT_3D('',#33420,#11654,#11655);
#9709=AXIS2_PLACEMENT_3D('',#33428,#11656,#11657);
#9710=AXIS2_PLACEMENT_3D('',#34331,#11658,#11659);
#9711=AXIS2_PLACEMENT_3D('',#34344,#11666,#11667);
#9712=AXIS2_PLACEMENT_3D('',#34345,#11668,#11669);
#9713=AXIS2_PLACEMENT_3D('',#34351,#11673,#11674);
#9714=AXIS2_PLACEMENT_3D('',#34355,#11677,#11678);
#9715=AXIS2_PLACEMENT_3D('',#34359,#11681,#11682);
#9716=AXIS2_PLACEMENT_3D('',#34363,#11685,#11686);
#9717=AXIS2_PLACEMENT_3D('',#34367,#11689,#11690);
#9718=AXIS2_PLACEMENT_3D('',#34369,#11692,#11693);
#11622=DIRECTION('axis',(0.,0.,1.));
#11623=DIRECTION('refdir',(1.,0.,0.));
#11624=DIRECTION('center_axis',(0.,0.,1.));
#11625=DIRECTION('ref_axis',(-0.349613253226052,-0.936894109901805,0.));
#11626=DIRECTION('',(0.,0.,1.));
#11627=DIRECTION('center_axis',(0.,0.,-1.));
#11628=DIRECTION('ref_axis',(1.,0.,0.));
#11629=DIRECTION('center_axis',(0.,0.,1.));
#11630=DIRECTION('ref_axis',(1.,0.,0.));
#11631=DIRECTION('',(0.,0.,1.));
#11632=DIRECTION('center_axis',(0.,0.,1.));
#11633=DIRECTION('ref_axis',(1.,0.,0.));
#11634=DIRECTION('',(0.,0.,1.));
#11635=DIRECTION('center_axis',(0.,0.,1.));
#11636=DIRECTION('ref_axis',(0.936891223524395,0.349620988047003,0.));
#11637=DIRECTION('',(0.,0.,1.));
#11638=DIRECTION('center_axis',(0.,0.,-1.));
#11639=DIRECTION('ref_axis',(1.,0.,0.));
#11640=DIRECTION('center_axis',(0.,0.,1.));
#11641=DIRECTION('ref_axis',(1.,3.79078190120237E-16,0.));
#11642=DIRECTION('',(1.22464679914735E-16,6.14212870423506E-32,1.));
#11643=DIRECTION('center_axis',(0.,0.,-1.));
#11644=DIRECTION('ref_axis',(1.,3.79078190120237E-16,0.));
#11645=DIRECTION('center_axis',(0.,0.,1.));
#11646=DIRECTION('ref_axis',(1.,3.79078190120237E-16,0.));
#11647=DIRECTION('',(1.22464679914735E-16,6.14212870423506E-32,1.));
#11648=DIRECTION('center_axis',(0.,0.,1.));
#11649=DIRECTION('ref_axis',(1.,3.79078190120237E-16,0.));
#11650=DIRECTION('',(1.22464679914735E-16,6.14212870423506E-32,1.));
#11651=DIRECTION('center_axis',(0.,0.,1.));
#11652=DIRECTION('ref_axis',(-0.608868629140097,0.79327107122916,0.));
#11653=DIRECTION('',(1.22464679914735E-16,6.14212870423506E-32,1.));
#11654=DIRECTION('center_axis',(0.,0.,1.));
#11655=DIRECTION('ref_axis',(1.,3.79078190120237E-16,0.));
#11656=DIRECTION('center_axis',(0.,0.,1.));
#11657=DIRECTION('ref_axis',(1.,3.79078190120237E-16,0.));
#11658=DIRECTION('center_axis',(0.,0.,1.));
#11659=DIRECTION('ref_axis',(1.,0.,0.));
#11660=DIRECTION('',(0.5,0.866025403784439,0.));
#11661=DIRECTION('',(-0.5,0.866025403784439,0.));
#11662=DIRECTION('',(-1.,0.,0.));
#11663=DIRECTION('',(-0.5,-0.866025403784439,0.));
#11664=DIRECTION('',(0.499999999999999,-0.866025403784439,0.));
#11665=DIRECTION('',(1.,-2.13662520709285E-16,0.));
#11666=DIRECTION('center_axis',(0.,0.,1.));
#11667=DIRECTION('ref_axis',(1.,0.,0.));
#11668=DIRECTION('center_axis',(-2.13662520709285E-16,-1.,0.));
#11669=DIRECTION('ref_axis',(1.,-2.13662520709285E-16,0.));
#11670=DIRECTION('',(1.,-2.13662520709285E-16,0.));
#11671=DIRECTION('',(0.,0.,1.));
#11672=DIRECTION('',(0.,0.,1.));
#11673=DIRECTION('center_axis',(-0.866025403784439,-0.499999999999999,0.));
#11674=DIRECTION('ref_axis',(0.499999999999999,-0.866025403784439,0.));
#11675=DIRECTION('',(0.499999999999999,-0.866025403784439,0.));
#11676=DIRECTION('',(0.,0.,1.));
#11677=DIRECTION('center_axis',(-0.866025403784439,0.5,0.));
#11678=DIRECTION('ref_axis',(-0.5,-0.866025403784439,0.));
#11679=DIRECTION('',(-0.5,-0.866025403784439,0.));
#11680=DIRECTION('',(0.,0.,1.));
#11681=DIRECTION('center_axis',(0.,1.,0.));
#11682=DIRECTION('ref_axis',(-1.,0.,0.));
#11683=DIRECTION('',(-1.,0.,0.));
#11684=DIRECTION('',(0.,0.,1.));
#11685=DIRECTION('center_axis',(0.866025403784439,0.5,0.));
#11686=DIRECTION('ref_axis',(-0.5,0.866025403784439,0.));
#11687=DIRECTION('',(-0.5,0.866025403784439,0.));
#11688=DIRECTION('',(0.,0.,1.));
#11689=DIRECTION('center_axis',(0.866025403784439,-0.5,0.));
#11690=DIRECTION('ref_axis',(0.5,0.866025403784439,0.));
#11691=DIRECTION('',(0.5,0.866025403784439,0.));
#11692=DIRECTION('center_axis',(0.,0.,1.));
#11693=DIRECTION('ref_axis',(1.,0.,0.));
#33015=CARTESIAN_POINT('',(0.,0.,0.));
#33016=CARTESIAN_POINT('Origin',(-8.5,0.,25.1));
#33017=CARTESIAN_POINT('',(-9.55012868473597,-2.18483901666677E-5,26.2841069671524));
#33018=CARTESIAN_POINT('',(-9.55000808233714,1.77385175400095E-6,26.3658930328476));
#33019=CARTESIAN_POINT('',(-9.5501,-1.28600160378464E-16,25.1));
#33020=CARTESIAN_POINT('',(-9.29338130674011,-0.687936125025682,26.4));
#33021=CARTESIAN_POINT('Ctrl Pts',(-9.55000808233714,1.77385175400095E-6,
26.3658930328476));
#33022=CARTESIAN_POINT('Ctrl Pts',(-9.55001544756934,-0.0803124474913518,
26.3695440482821));
#33023=CARTESIAN_POINT('Ctrl Pts',(-9.54090375927775,-0.160621737063475,
26.3731950637165));
#33024=CARTESIAN_POINT('Ctrl Pts',(-9.52264585408719,-0.238788344862009,
26.3768460791509));
#33025=CARTESIAN_POINT('Ctrl Pts',(-9.48405000778592,-0.404026708682781,
26.3845640527673));
#33026=CARTESIAN_POINT('Ctrl Pts',(-9.4045826463392,-0.559690113640417,
26.3922820263836));
#33027=CARTESIAN_POINT('Ctrl Pts',(-9.29338130674012,-0.687936125025676,
26.4));
#33028=CARTESIAN_POINT('',(-7.7065804240351,-0.68794180318535,26.4));
#33029=CARTESIAN_POINT('Origin',(-8.5,0.,26.4));
#33030=CARTESIAN_POINT('Ctrl Pts',(-7.7065804240351,-0.68794180318535,26.4));
#33031=CARTESIAN_POINT('Ctrl Pts',(-7.79864112035199,-0.793916326566851,
26.3936166544345));
#33032=CARTESIAN_POINT('Ctrl Pts',(-7.91206794128119,-0.881431589437098,
26.387233308869));
#33033=CARTESIAN_POINT('Ctrl Pts',(-8.0381219127883,-0.94316142252496,26.3808499633034));
#33034=CARTESIAN_POINT('Ctrl Pts',(-8.19053121232317,-1.01779771132126,
26.3731319896871));
#33035=CARTESIAN_POINT('Ctrl Pts',(-8.36139981181721,-1.05473895720253,
26.3654140160707));
#33036=CARTESIAN_POINT('Ctrl Pts',(-8.53102866379217,-1.04972498576314,
26.3576960424544));
#33037=CARTESIAN_POINT('Ctrl Pts',(-8.70065751576713,-1.04471101432375,
26.349978068838));
#33038=CARTESIAN_POINT('Ctrl Pts',(-8.869046620223,-0.997741825563708,26.3422600952216));
#33039=CARTESIAN_POINT('Ctrl Pts',(-9.01678108566738,-0.914233151702619,
26.3345421216053));
#33040=CARTESIAN_POINT('Ctrl Pts',(-9.16451555111177,-0.830724477841526,
26.3268241479889));
#33041=CARTESIAN_POINT('Ctrl Pts',(-9.29159537754465,-0.710676318879388,
26.3191061743726));
#33042=CARTESIAN_POINT('Ctrl Pts',(-9.38336919906597,-0.567929359810613,
26.3113882007562));
#33043=CARTESIAN_POINT('Ctrl Pts',(-9.47514302058727,-0.425182400741845,
26.3036702271398));
#33044=CARTESIAN_POINT('Ctrl Pts',(-9.53161083719701,-0.259736641566442,
26.2959522535235));
#33045=CARTESIAN_POINT('Ctrl Pts',(-9.54626210360576,-0.0906671713680419,
26.2882342799071));
#33046=CARTESIAN_POINT('Ctrl Pts',(-9.54887377180294,-0.0605296156023525,
26.2868585089889));
#33047=CARTESIAN_POINT('Ctrl Pts',(-9.55015671877703,-0.0302769163894044,
26.2854827380706));
#33048=CARTESIAN_POINT('Ctrl Pts',(-9.55012868473597,-2.18483901666677E-5,
26.2841069671524));
#33049=CARTESIAN_POINT('Origin',(-8.5,0.,25.1));
#33050=CARTESIAN_POINT('',(-9.55014863741965,-1.85392332084922E-5,25.9841069671524));
#33051=CARTESIAN_POINT('',(-9.55002929519846,-9.63122723742732E-6,26.0658930328476));
#33052=CARTESIAN_POINT('',(-9.5501,-1.28600160378464E-16,25.1));
#33053=CARTESIAN_POINT('Ctrl Pts',(-9.55002929519846,-9.63122723742732E-6,
26.0658930328476));
#33054=CARTESIAN_POINT('Ctrl Pts',(-9.55005413296486,-0.0729827234261202,
26.0692103912693));
#33055=CARTESIAN_POINT('Ctrl Pts',(-9.54254682320219,-0.145950776385278,
26.0725277496911));
#33056=CARTESIAN_POINT('Ctrl Pts',(-9.5274529085174,-0.21731420414845,26.0758451081128));
#33057=CARTESIAN_POINT('Ctrl Pts',(-9.49233628242652,-0.383344214364866,
26.0835630817291));
#33058=CARTESIAN_POINT('Ctrl Pts',(-9.41615489969101,-0.540688713228667,
26.0912810553455));
#33059=CARTESIAN_POINT('Ctrl Pts',(-9.3076920597651,-0.671206733850008,
26.0989990289619));
#33060=CARTESIAN_POINT('Ctrl Pts',(-9.19922921983919,-0.801724754471348,
26.1067170025782));
#33061=CARTESIAN_POINT('Ctrl Pts',(-9.05848492272286,-0.905416296850228,
26.1144349761946));
#33062=CARTESIAN_POINT('Ctrl Pts',(-8.90168621780771,-0.970326296905908,
26.1221529498109));
#33063=CARTESIAN_POINT('Ctrl Pts',(-8.74488751289256,-1.03523629696159,
26.1298709234273));
#33064=CARTESIAN_POINT('Ctrl Pts',(-8.57203440017859,-1.06136475469407,
26.1375888970437));
#33065=CARTESIAN_POINT('Ctrl Pts',(-8.40305590625563,-1.04569918755626,
26.14530687066));
#33066=CARTESIAN_POINT('Ctrl Pts',(-8.23407741233268,-1.03003362041845,
26.1530248442764));
#33067=CARTESIAN_POINT('Ctrl Pts',(-8.06897353720075,-0.972574028410342,
26.1607428178928));
#33068=CARTESIAN_POINT('Ctrl Pts',(-7.92677985019183,-0.879945219242199,
26.1684607915091));
#33069=CARTESIAN_POINT('Ctrl Pts',(-7.78458616318292,-0.787316410074058,
26.1761787651255));
#33070=CARTESIAN_POINT('Ctrl Pts',(-7.66530266429701,-0.659518383745877,
26.1838967387419));
#33071=CARTESIAN_POINT('Ctrl Pts',(-7.58268210950511,-0.511285491489167,
26.1916147123582));
#33072=CARTESIAN_POINT('Ctrl Pts',(-7.50006155471321,-0.363052599232457,
26.1993326859746));
#33073=CARTESIAN_POINT('Ctrl Pts',(-7.45410394401532,-0.194384841047217,
26.2070506595909));
#33074=CARTESIAN_POINT('Ctrl Pts',(-7.45010789815323,-0.0247288321007086,
26.2147686332073));
#33075=CARTESIAN_POINT('Ctrl Pts',(-7.44611185229113,0.144927176845799,
26.2224866068237));
#33076=CARTESIAN_POINT('Ctrl Pts',(-7.48407737126484,0.315571436553571,
26.23020458044));
#33077=CARTESIAN_POINT('Ctrl Pts',(-7.55962732154007,0.467529907730423,
26.2379225540564));
#33078=CARTESIAN_POINT('Ctrl Pts',(-7.63517727181531,0.619488378907277,
26.2456405276728));
#33079=CARTESIAN_POINT('Ctrl Pts',(-7.74831165339208,0.752761061553206,
26.2533585012891));
#33080=CARTESIAN_POINT('Ctrl Pts',(-7.88598648304016,0.851981672429286,
26.2610764749055));
#33081=CARTESIAN_POINT('Ctrl Pts',(-8.02366131268824,0.951202283305365,
26.2687944485219));
#33082=CARTESIAN_POINT('Ctrl Pts',(-8.18587659040763,1.0163708224116,26.2765124221382));
#33083=CARTESIAN_POINT('Ctrl Pts',(-8.35393016091651,1.03997523612929,26.2842303957546));
#33084=CARTESIAN_POINT('Ctrl Pts',(-8.52198373142539,1.06357964984699,26.2919483693709));
#33085=CARTESIAN_POINT('Ctrl Pts',(-8.69587559472376,1.04561993817614,26.2996663429873));
#33086=CARTESIAN_POINT('Ctrl Pts',(-8.85555592518767,0.988163616219066,
26.3073843166036));
#33087=CARTESIAN_POINT('Ctrl Pts',(-9.01523625565157,0.93070729426199,26.31510229022));
#33088=CARTESIAN_POINT('Ctrl Pts',(-9.160705053281,0.833754362018685,26.3228202638364));
#33089=CARTESIAN_POINT('Ctrl Pts',(-9.27519220406066,0.708490434988905,
26.3305382374527));
#33090=CARTESIAN_POINT('Ctrl Pts',(-9.38967935484033,0.583226507959125,
26.3382562110691));
#33091=CARTESIAN_POINT('Ctrl Pts',(-9.47318485877022,0.42965158614287,26.3459741846855));
#33092=CARTESIAN_POINT('Ctrl Pts',(-9.51607544515725,0.265457463892782,
26.3536921583018));
#33093=CARTESIAN_POINT('Ctrl Pts',(-9.53867648396682,0.178935967175755,
26.3577591164838));
#33094=CARTESIAN_POINT('Ctrl Pts',(-9.54999987801921,0.0894658107705327,
26.3618260746657));
#33095=CARTESIAN_POINT('Ctrl Pts',(-9.55000808233714,1.77385175400095E-6,
26.3658930328476));
#33096=CARTESIAN_POINT('Ctrl Pts',(-9.55012868473597,-2.18483901666677E-5,
26.2841069671524));
#33097=CARTESIAN_POINT('Ctrl Pts',(-9.54999944986955,0.139451788792166,
26.2777647644543));
#33098=CARTESIAN_POINT('Ctrl Pts',(-9.52201000479389,0.278975766050527,
26.2714225617561));
#33099=CARTESIAN_POINT('Ctrl Pts',(-9.46789831314616,0.407501832957038,
26.265080359058));
#33100=CARTESIAN_POINT('Ctrl Pts',(-9.40204854007008,0.563908185862314,
26.2573623854417));
#33101=CARTESIAN_POINT('Ctrl Pts',(-9.29751427771017,0.704027710451462,
26.2496444118253));
#33102=CARTESIAN_POINT('Ctrl Pts',(-9.16634773368461,0.811705368632605,
26.2419264382089));
#33103=CARTESIAN_POINT('Ctrl Pts',(-9.03518118965904,0.919383026813746,
26.2342084645926));
#33104=CARTESIAN_POINT('Ctrl Pts',(-8.87738236396781,0.994618818586882,
26.2264904909762));
#33105=CARTESIAN_POINT('Ctrl Pts',(-8.7111446128674,1.028738475975,26.2187725173598));
#33106=CARTESIAN_POINT('Ctrl Pts',(-8.54490686176699,1.06285813336311,26.2110545437435));
#33107=CARTESIAN_POINT('Ctrl Pts',(-8.3702301852574,1.05586165636621,26.2033365701271));
#33108=CARTESIAN_POINT('Ctrl Pts',(-8.20725384815146,1.0085556965313,26.1956185965107));
#33109=CARTESIAN_POINT('Ctrl Pts',(-8.04427751104553,0.961249736696391,
26.1879006228944));
#33110=CARTESIAN_POINT('Ctrl Pts',(-7.89300151334325,0.873634294023485,
26.180182649278));
#33111=CARTESIAN_POINT('Ctrl Pts',(-7.77086715620623,0.755810953939201,
26.1724646756617));
#33112=CARTESIAN_POINT('Ctrl Pts',(-7.64873279906922,0.637987613854915,
26.1647467020453));
#33113=CARTESIAN_POINT('Ctrl Pts',(-7.55574008249746,0.489956376359252,
26.1570287284289));
#33114=CARTESIAN_POINT('Ctrl Pts',(-7.50261055937172,0.328784436297264,
26.1493107548126));
#33115=CARTESIAN_POINT('Ctrl Pts',(-7.44948103624598,0.167612496235276,
26.1415927811962));
#33116=CARTESIAN_POINT('Ctrl Pts',(-7.43621470656625,-0.00670014639303557,
26.1338748075799));
#33117=CARTESIAN_POINT('Ctrl Pts',(-7.46434110638773,-0.174056192550768,
26.1261568339635));
#33118=CARTESIAN_POINT('Ctrl Pts',(-7.49246750620921,-0.341412238708501,
26.1184388603471));
#33119=CARTESIAN_POINT('Ctrl Pts',(-7.5619866355319,-0.501811688395654,
26.1107208867308));
#33120=CARTESIAN_POINT('Ctrl Pts',(-7.66488331703068,-0.636761358552236,
26.1030029131144));
#33121=CARTESIAN_POINT('Ctrl Pts',(-7.76777999852946,-0.771711028708818,
26.095284939498));
#33122=CARTESIAN_POINT('Ctrl Pts',(-7.90405423220433,-0.881210919334829,
26.0875669658817));
#33123=CARTESIAN_POINT('Ctrl Pts',(-8.05799434096646,-0.952636289137738,
26.0798489922653));
#33124=CARTESIAN_POINT('Ctrl Pts',(-8.2119344497286,-1.02406165894065,26.072131018649));
#33125=CARTESIAN_POINT('Ctrl Pts',(-8.38354043357801,-1.05741250792046,
26.0644130450326));
#33126=CARTESIAN_POINT('Ctrl Pts',(-8.55302705685301,-1.04884366480909,
26.0566950714162));
#33127=CARTESIAN_POINT('Ctrl Pts',(-8.72251368012801,-1.04027482169772,
26.0489770977999));
#33128=CARTESIAN_POINT('Ctrl Pts',(-8.88988094282861,-0.989786286495173,
26.0412591241835));
#33129=CARTESIAN_POINT('Ctrl Pts',(-9.03583231082944,-0.903199112404309,
26.0335411505671));
#33130=CARTESIAN_POINT('Ctrl Pts',(-9.18178367883027,-0.816611938313444,
26.0258231769508));
#33131=CARTESIAN_POINT('Ctrl Pts',(-9.30631915213132,-0.693926125334262,
26.0181052033344));
#33132=CARTESIAN_POINT('Ctrl Pts',(-9.39508046869405,-0.549286679739332,
26.0103872297181));
#33133=CARTESIAN_POINT('Ctrl Pts',(-9.48384178525678,-0.404647234144403,
26.0026692561017));
#33134=CARTESIAN_POINT('Ctrl Pts',(-9.53682894508118,-0.238054155933727,
25.9949512824853));
#33135=CARTESIAN_POINT('Ctrl Pts',(-9.54793281713632,-0.0687147199931099,
25.987233308869));
#33136=CARTESIAN_POINT('Ctrl Pts',(-9.54943210957357,-0.045849782935783,
25.9861911949634));
#33137=CARTESIAN_POINT('Ctrl Pts',(-9.55016780438665,-0.0229347754959868,
25.9851490810579));
#33138=CARTESIAN_POINT('Ctrl Pts',(-9.55014863741965,-1.85392332084922E-5,
25.9841069671524));
#33139=CARTESIAN_POINT('Origin',(-8.5,0.,25.1));
#33140=CARTESIAN_POINT('',(-9.5501656695242,-1.36966039699926E-5,25.6841069671524));
#33141=CARTESIAN_POINT('',(-9.55003919466624,-1.48519393190782E-5,25.7658930328476));
#33142=CARTESIAN_POINT('',(-9.5501,-1.28600160378464E-16,25.1));
#33143=CARTESIAN_POINT('Ctrl Pts',(-9.55003919466624,-1.48519393190782E-5,
25.7658930328476));
#33144=CARTESIAN_POINT('Ctrl Pts',(-9.55007410770739,-0.0656465986864928,
25.7688767342566));
#33145=CARTESIAN_POINT('Ctrl Pts',(-9.54400992574163,-0.13127197210093,
25.7718604356656));
#33146=CARTESIAN_POINT('Ctrl Pts',(-9.53178263717497,-0.195728209905797,
25.7748441370746));
#33147=CARTESIAN_POINT('Ctrl Pts',(-9.50015417386016,-0.362457877052181,
25.782562110691));
#33148=CARTESIAN_POINT('Ctrl Pts',(-9.42728790559935,-0.521364770823876,
25.7902800843074));
#33149=CARTESIAN_POINT('Ctrl Pts',(-9.32158491639723,-0.654127791549347,
25.7979980579237));
#33150=CARTESIAN_POINT('Ctrl Pts',(-9.21588192719511,-0.786890812274816,
25.8057160315401));
#33151=CARTESIAN_POINT('Ctrl Pts',(-9.07734221705168,-0.89350995995406,
25.8134340051565));
#33152=CARTESIAN_POINT('Ctrl Pts',(-8.92193866025693,-0.9616926273552,25.8211519787728));
#33153=CARTESIAN_POINT('Ctrl Pts',(-8.76653510346219,-1.02987529475634,
25.8288699523892));
#33154=CARTESIAN_POINT('Ctrl Pts',(-8.59426770001613,-1.05962148187937,
25.8365879260055));
#33155=CARTESIAN_POINT('Ctrl Pts',(-8.42499794361343,-1.04750161530483,
25.8443058996219));
#33156=CARTESIAN_POINT('Ctrl Pts',(-8.25572818721072,-1.03538174873029,
25.8520238732383));
#33157=CARTESIAN_POINT('Ctrl Pts',(-8.08945607785137,-0.981395828458169,
25.8597418468546));
#33158=CARTESIAN_POINT('Ctrl Pts',(-7.94535188446413,-0.891768137164413,
25.867459820471));
#33159=CARTESIAN_POINT('Ctrl Pts',(-7.80124769107689,-0.802140445870657,
25.8751777940874));
#33160=CARTESIAN_POINT('Ctrl Pts',(-7.67931141366176,-0.676870983555263,
25.8828957677037));
#33161=CARTESIAN_POINT('Ctrl Pts',(-7.593601641113,-0.530402637186899,25.8906137413201));
#33162=CARTESIAN_POINT('Ctrl Pts',(-7.50789186856424,-0.383934290818535,
25.8983317149364));
#33163=CARTESIAN_POINT('Ctrl Pts',(-7.45840860088185,-0.216267060397201,
25.9060496885528));
#33164=CARTESIAN_POINT('Ctrl Pts',(-7.45085698941586,-0.0467320647085198,
25.9137676621692));
#33165=CARTESIAN_POINT('Ctrl Pts',(-7.44330537794987,0.122802930980162,
25.9214856357855));
#33166=CARTESIAN_POINT('Ctrl Pts',(-7.47768542270028,0.294205691936192,
25.9292036094019));
#33167=CARTESIAN_POINT('Ctrl Pts',(-7.55003329168869,0.447714413024386,
25.9369215830183));
#33168=CARTESIAN_POINT('Ctrl Pts',(-7.62238116067709,0.601223134112577,
25.9446395566346));
#33169=CARTESIAN_POINT('Ctrl Pts',(-7.73269685390349,0.736837815332934,
25.952357530251));
#33170=CARTESIAN_POINT('Ctrl Pts',(-7.8682615725681,0.838922822330773,25.9600755038674));
#33171=CARTESIAN_POINT('Ctrl Pts',(-8.00382629123272,0.941007829328613,
25.9677934774837));
#33172=CARTESIAN_POINT('Ctrl Pts',(-8.16464003533555,1.00956316210393,25.9755114511001));
#33173=CARTESIAN_POINT('Ctrl Pts',(-8.33216185572768,1.03668476398556,25.9832294247164));
#33174=CARTESIAN_POINT('Ctrl Pts',(-8.49968367611981,1.06380636586718,25.9909473983328));
#33175=CARTESIAN_POINT('Ctrl Pts',(-8.67391357280124,1.04949423685511,25.9986653719492));
#33176=CARTESIAN_POINT('Ctrl Pts',(-8.83476378732716,0.995398487625139,
26.0063833455655));
#33177=CARTESIAN_POINT('Ctrl Pts',(-8.99561400185307,0.941302738395167,
26.0141013191819));
#33178=CARTESIAN_POINT('Ctrl Pts',(-9.14308453422347,0.847423368947298,
26.0218192927982));
#33179=CARTESIAN_POINT('Ctrl Pts',(-9.26017283489315,0.724584159174464,
26.0295372664146));
#33180=CARTESIAN_POINT('Ctrl Pts',(-9.37726113556284,0.60174494940163,26.037255240031));
#33181=CARTESIAN_POINT('Ctrl Pts',(-9.4639672045318,0.449945899303832,26.0449732136473));
#33182=CARTESIAN_POINT('Ctrl Pts',(-9.51029430429316,0.286688613470416,
26.0526911872637));
#33183=CARTESIAN_POINT('Ctrl Pts',(-9.53670897597608,0.193602976179322,
26.0570918024583));
#33184=CARTESIAN_POINT('Ctrl Pts',(-9.54999634685876,0.0967922386666701,
26.061492417653));
#33185=CARTESIAN_POINT('Ctrl Pts',(-9.55002929519846,-9.63122723742732E-6,
26.0658930328476));
#33186=CARTESIAN_POINT('Ctrl Pts',(-9.55014863741965,-1.85392332084922E-5,
25.9841069671524));
#33187=CARTESIAN_POINT('Ctrl Pts',(-9.55002585239389,0.146784586201418,
25.9774311074416));
#33188=CARTESIAN_POINT('Ctrl Pts',(-9.51892520411974,0.293638139822104,
25.9707552477307));
#33189=CARTESIAN_POINT('Ctrl Pts',(-9.45914326904298,0.427702105940413,
25.9640793880199));
#33190=CARTESIAN_POINT('Ctrl Pts',(-9.39002926460864,0.582693702262755,
25.9563614144035));
#33191=CARTESIAN_POINT('Ctrl Pts',(-9.28258067145411,0.72059110123688,25.9486434407872));
#33192=CARTESIAN_POINT('Ctrl Pts',(-9.14918572735926,0.825495483554338,
25.9409254671708));
#33193=CARTESIAN_POINT('Ctrl Pts',(-9.01579078326441,0.930399865871797,
25.9332074935544));
#33194=CARTESIAN_POINT('Ctrl Pts',(-8.85644948822923,1.00231123153259,25.9254895199381));
#33195=CARTESIAN_POINT('Ctrl Pts',(-8.6895330260255,1.03293859160238,25.9177715463217));
#33196=CARTESIAN_POINT('Ctrl Pts',(-8.52261656382178,1.06356595167218,25.9100535727053));
#33197=CARTESIAN_POINT('Ctrl Pts',(-8.3481249344495,1.05290930615098,25.902335599089));
#33198=CARTESIAN_POINT('Ctrl Pts',(-8.18617607274301,1.00219730824664,25.8946176254726));
#33199=CARTESIAN_POINT('Ctrl Pts',(-8.02422721103653,0.951485310342298,
25.8868996518563));
#33200=CARTESIAN_POINT('Ctrl Pts',(-7.87482111699583,0.860717960054822,
25.8791816782399));
#33201=CARTESIAN_POINT('Ctrl Pts',(-7.75518349981129,0.740360238682796,
25.8714637046235));
#33202=CARTESIAN_POINT('Ctrl Pts',(-7.63554588262674,0.62000251731077,25.8637457310072));
#33203=CARTESIAN_POINT('Ctrl Pts',(-7.54567674229835,0.470054424854194,
25.8560277573908));
#33204=CARTESIAN_POINT('Ctrl Pts',(-7.49593750140689,0.307804159969934,
25.8483097837744));
#33205=CARTESIAN_POINT('Ctrl Pts',(-7.44619826051544,0.145553895085674,
25.8405918101581));
#33206=CARTESIAN_POINT('Ctrl Pts',(-7.43658891906092,-0.028998542226271,
25.8328738365417));
#33207=CARTESIAN_POINT('Ctrl Pts',(-7.46821738179425,-0.195728206307347,
25.8251558629254));
#33208=CARTESIAN_POINT('Ctrl Pts',(-7.49984584452757,-0.362457870388421,
25.817437889309));
#33209=CARTESIAN_POINT('Ctrl Pts',(-7.57271211144874,-0.521364761238627,
25.8097199156926));
#33210=CARTESIAN_POINT('Ctrl Pts',(-7.67841509870752,-0.654127779523261,
25.8020019420763));
#33211=CARTESIAN_POINT('Ctrl Pts',(-7.7841180859663,-0.786890797807898,
25.7942839684599));
#33212=CARTESIAN_POINT('Ctrl Pts',(-7.92265779356269,-0.893509943526962,
25.7865659948435));
#33213=CARTESIAN_POINT('Ctrl Pts',(-8.07806134750036,-0.961692609674572,
25.7788480212272));
#33214=CARTESIAN_POINT('Ctrl Pts',(-8.23346490143802,-1.02987527582218,
25.7711300476108));
#33215=CARTESIAN_POINT('Ctrl Pts',(-8.40573230171696,-1.05962146239834,
25.7634120739945));
#33216=CARTESIAN_POINT('Ctrl Pts',(-8.57500205500766,-1.04750159604662,
25.7556941003781));
#33217=CARTESIAN_POINT('Ctrl Pts',(-8.74427180829836,-1.0353817296949,25.7479761267617));
#33218=CARTESIAN_POINT('Ctrl Pts',(-8.91054391460082,-0.981395810415311,
25.7402581531454));
#33219=CARTESIAN_POINT('Ctrl Pts',(-9.05464810533871,-0.891768120769351,
25.732540179529));
#33220=CARTESIAN_POINT('Ctrl Pts',(-9.19875229607661,-0.802140431123391,
25.7248222059126));
#33221=CARTESIAN_POINT('Ctrl Pts',(-9.32068857124995,-0.676870971111062,
25.7171042322963));
#33222=CARTESIAN_POINT('Ctrl Pts',(-9.40639834222295,-0.530402627435509,
25.7093862586799));
#33223=CARTESIAN_POINT('Ctrl Pts',(-9.49210811319594,-0.383934283759956,
25.7016682850636));
#33224=CARTESIAN_POINT('Ctrl Pts',(-9.54159137996859,-0.216267056421179,
25.6939503114472));
#33225=CARTESIAN_POINT('Ctrl Pts',(-9.54914299129575,-0.0467320638493777,
25.6862323378308));
#33226=CARTESIAN_POINT('Ctrl Pts',(-9.54983617727468,-0.0311699176136354,
25.685523880938));
#33227=CARTESIAN_POINT('Ctrl Pts',(-9.55017604807986,-0.0155920336305797,
25.6848154240452));
#33228=CARTESIAN_POINT('Ctrl Pts',(-9.5501656695242,-1.36966039699926E-5,
25.6841069671524));
#33229=CARTESIAN_POINT('Origin',(-8.5,0.,25.1));
#33230=CARTESIAN_POINT('',(-9.55017788167088,-7.61182092967605E-6,25.3841069671524));
#33231=CARTESIAN_POINT('',(-9.55005314880761,-1.91003690738122E-5,25.4658930328476));
#33232=CARTESIAN_POINT('',(-9.5501,-1.28600160378464E-16,25.1));
#33233=CARTESIAN_POINT('',(-7.70661869325988,-0.68793612502568,25.2));
#33234=CARTESIAN_POINT('Ctrl Pts',(-9.55017788167088,-7.61182092967605E-6,
25.3841069671524));
#33235=CARTESIAN_POINT('Ctrl Pts',(-9.55011213443803,0.161456744878573,
25.3767637934161));
#33236=CARTESIAN_POINT('Ctrl Pts',(-9.51225375626492,0.322950830145204,
25.3694206196799));
#33237=CARTESIAN_POINT('Ctrl Pts',(-9.44037266037286,0.467529898294161,
25.3620774459436));
#33238=CARTESIAN_POINT('Ctrl Pts',(-9.36482271132683,0.619488366598228,
25.3543594723273));
#33239=CARTESIAN_POINT('Ctrl Pts',(-9.25168833177352,0.752761047051947,
25.3466414987109));
#33240=CARTESIAN_POINT('Ctrl Pts',(-9.11401350383482,0.851981655213685,
25.3389235250945));
#33241=CARTESIAN_POINT('Ctrl Pts',(-8.97633867589611,0.951202263375423,
25.3312055514782));
#33242=CARTESIAN_POINT('Ctrl Pts',(-8.814123399572,1.01637079924518,25.3234875778618));
#33243=CARTESIAN_POINT('Ctrl Pts',(-8.64606983101463,1.03997521165314,25.3157696042454));
#33244=CARTESIAN_POINT('Ctrl Pts',(-8.47801626245725,1.06357962406111,25.3080516306291));
#33245=CARTESIAN_POINT('Ctrl Pts',(-8.30412440166661,1.04561991300728,25.3003336570127));
#33246=CARTESIAN_POINT('Ctrl Pts',(-8.1444440694765,0.988163587521729,25.2926156833963));
#33247=CARTESIAN_POINT('Ctrl Pts',(-7.98476373728639,0.930707262036181,
25.28489770978));
#33248=CARTESIAN_POINT('Ctrl Pts',(-7.83929493369681,0.833754322118917,
25.2771797361636));
#33249=CARTESIAN_POINT('Ctrl Pts',(-7.72480777961413,0.708490392601629,
25.2694617625473));
#33250=CARTESIAN_POINT('Ctrl Pts',(-7.61032062553146,0.583226463084341,
25.2617437889309));
#33251=CARTESIAN_POINT('Ctrl Pts',(-7.5268151209557,0.429651543967029,25.2540258153145));
#33252=CARTESIAN_POINT('Ctrl Pts',(-7.48392451805012,0.265457409338225,
25.2463078416982));
#33253=CARTESIAN_POINT('Ctrl Pts',(-7.44103391514455,0.101263274709422,
25.2385898680818));
#33254=CARTESIAN_POINT('Ctrl Pts',(-7.43875821390916,-0.0735500754308729,
25.2308718944654));
#33255=CARTESIAN_POINT('Ctrl Pts',(-7.47735407353822,-0.238788422518332,
25.2231539208491));
#33256=CARTESIAN_POINT('Ctrl Pts',(-7.51594993316728,-0.404026769605792,
25.2154359472327));
#33257=CARTESIAN_POINT('Ctrl Pts',(-7.59541735366079,-0.559690113640417,
25.2077179736164));
#33258=CARTESIAN_POINT('Ctrl Pts',(-7.70661869325989,-0.687936125025681,
25.2));
#33259=CARTESIAN_POINT('',(-9.29341958724171,-0.687941828405758,25.2));
#33260=CARTESIAN_POINT('Origin',(-8.5,0.,25.2));
#33261=CARTESIAN_POINT('Ctrl Pts',(-9.29341958724171,-0.687941828405758,
25.2));
#33262=CARTESIAN_POINT('Ctrl Pts',(-9.20135889014717,-0.793916350040231,
25.2063833455655));
#33263=CARTESIAN_POINT('Ctrl Pts',(-9.08793206769768,-0.88143161422273,
25.212766691131));
#33264=CARTESIAN_POINT('Ctrl Pts',(-8.96187809424672,-0.943161447318046,
25.2191500366966));
#33265=CARTESIAN_POINT('Ctrl Pts',(-8.8094687923616,-1.01779773612335,25.2268680103129));
#33266=CARTESIAN_POINT('Ctrl Pts',(-8.63860018989813,-1.05473898010619,
25.2345859839293));
#33267=CARTESIAN_POINT('Ctrl Pts',(-8.46897133498624,-1.04972500737682,
25.2423039575456));
#33268=CARTESIAN_POINT('Ctrl Pts',(-8.29934248007435,-1.04471103464745,
25.250021931162));
#33269=CARTESIAN_POINT('Ctrl Pts',(-8.13095337271404,-0.997741845205878,
25.2577399047784));
#33270=CARTESIAN_POINT('Ctrl Pts',(-7.98321890464159,-0.91423316965448,
25.2654578783947));
#33271=CARTESIAN_POINT('Ctrl Pts',(-7.83548443656915,-0.830724494103082,
25.2731758520111));
#33272=CARTESIAN_POINT('Ctrl Pts',(-7.70840460778457,-0.710676332441859,
25.2808938256275));
#33273=CARTESIAN_POINT('Ctrl Pts',(-7.61663078459231,-0.567929370544709,
25.2886117992438));
#33274=CARTESIAN_POINT('Ctrl Pts',(-7.52485696140006,-0.425182408647558,
25.2963297728602));
#33275=CARTESIAN_POINT('Ctrl Pts',(-7.46838914380013,-0.25973664651448,
25.3040477464766));
#33276=CARTESIAN_POINT('Ctrl Pts',(-7.45373787713935,-0.0906671732020418,
25.3117657200929));
#33277=CARTESIAN_POINT('Ctrl Pts',(-7.43908661047857,0.0784023001103964,
25.3194836937093));
#33278=CARTESIAN_POINT('Ctrl Pts',(-7.46625189475693,0.251095484602196,
25.3272016673256));
#33279=CARTESIAN_POINT('Ctrl Pts',(-7.53210166904304,0.407501840417961,
25.334919640942));
#33280=CARTESIAN_POINT('Ctrl Pts',(-7.59795144332914,0.563908196233726,
25.3426376145584));
#33281=CARTESIAN_POINT('Ctrl Pts',(-7.70248570762299,0.704027723373456,
25.3503555881747));
#33282=CARTESIAN_POINT('Ctrl Pts',(-7.83365225406373,0.811705383531112,
25.3580735617911));
#33283=CARTESIAN_POINT('Ctrl Pts',(-7.96481880050447,0.919383043688767,
25.3657915354074));
#33284=CARTESIAN_POINT('Ctrl Pts',(-8.12261762909211,0.994618836864348,
25.3735095090238));
#33285=CARTESIAN_POINT('Ctrl Pts',(-8.28885538324795,1.02873849488606,25.3812274826402));
#33286=CARTESIAN_POINT('Ctrl Pts',(-8.45509313740379,1.06285815290777,25.3889454562565));
#33287=CARTESIAN_POINT('Ctrl Pts',(-8.62976981712784,1.05586167577561,25.3966634298729));
#33288=CARTESIAN_POINT('Ctrl Pts',(-8.79274615723093,1.00855571506968,25.4043814034893));
#33289=CARTESIAN_POINT('Ctrl Pts',(-8.95572249733401,0.961249754363756,
25.4120993771056));
#33290=CARTESIAN_POINT('Ctrl Pts',(-9.10699849781613,0.873634310084068,
25.419817350722));
#33291=CARTESIAN_POINT('Ctrl Pts',(-9.22913285719828,0.755810967834823,
25.4275353243384));
#33292=CARTESIAN_POINT('Ctrl Pts',(-9.35126721658042,0.637987625585578,
25.4352532979547));
#33293=CARTESIAN_POINT('Ctrl Pts',(-9.4442599348626,0.489956385366774,25.4429712715711));
#33294=CARTESIAN_POINT('Ctrl Pts',(-9.49738945896532,0.328784442341286,
25.4506892451874));
#33295=CARTESIAN_POINT('Ctrl Pts',(-9.53227642295773,0.222952518041617,
25.4557571744075));
#33296=CARTESIAN_POINT('Ctrl Pts',(-9.54997533738096,0.111454639072124,
25.4608251036276));
#33297=CARTESIAN_POINT('Ctrl Pts',(-9.55005314880761,-1.91003690738122E-5,
25.4658930328476));
#33298=CARTESIAN_POINT('Origin',(-8.5,0.,24.5374873996035));
#33299=CARTESIAN_POINT('',(-9.71736802727299,-1.11661151494524E-5,26.1625126003965));
#33300=CARTESIAN_POINT('',(-9.71748325610114,-2.53302756962299E-5,26.1874873996035));
#33301=CARTESIAN_POINT('',(-9.71745,-6.10603367124078E-16,24.5374873996035));
#33302=CARTESIAN_POINT('',(-8.18521110449559,1.17604951161383,26.4));
#33303=CARTESIAN_POINT('Ctrl Pts',(-9.71748325610114,-2.53302756962961E-5,
26.1874873996035));
#33304=CARTESIAN_POINT('Ctrl Pts',(-9.71751575780888,-0.0351020206249033,
26.1888631705217));
#33305=CARTESIAN_POINT('Ctrl Pts',(-9.7076841214477,-0.266938209970575,
26.1979569150563));
#33306=CARTESIAN_POINT('Ctrl Pts',(-9.56508058954619,-0.684754074175086,
26.2147686332073));
#33307=CARTESIAN_POINT('Ctrl Pts',(-9.12308458528742,-1.10229325462015,
26.2379225540564));
#33308=CARTESIAN_POINT('Ctrl Pts',(-8.53741089167782,-1.26565666435994,
26.2610764749055));
#33309=CARTESIAN_POINT('Ctrl Pts',(-7.94311327301097,-1.13717141591269,
26.2842303957546));
#33310=CARTESIAN_POINT('Ctrl Pts',(-7.47722213792833,-0.746472111678944,
26.3073843166037));
#33311=CARTESIAN_POINT('Ctrl Pts',(-7.24718515000566,-0.183635660921369,
26.3305382374527));
#33312=CARTESIAN_POINT('Ctrl Pts',(-7.30600772843461,0.421517288496708,
26.3536921583018));
#33313=CARTESIAN_POINT('Ctrl Pts',(-7.64021467375676,0.929507511744114,
26.3768460791509));
#33314=CARTESIAN_POINT('Ctrl Pts',(-7.99510874416174,1.12516550422186,26.3922820263836));
#33315=CARTESIAN_POINT('Ctrl Pts',(-8.1852111044956,1.17604951161383,26.4));
#33316=CARTESIAN_POINT('',(-8.81478889550438,1.17604951161383,26.4));
#33317=CARTESIAN_POINT('Origin',(-8.5,0.,26.4));
#33318=CARTESIAN_POINT('Ctrl Pts',(-9.71736802727299,-1.11661151495218E-5,
26.1625126003965));
#33319=CARTESIAN_POINT('Ctrl Pts',(-9.71739682332927,-0.0846136716837212,
26.1658299588182));
#33320=CARTESIAN_POINT('Ctrl Pts',(-9.68844354006211,-0.366028022972056,
26.1768652908563));
#33321=CARTESIAN_POINT('Ctrl Pts',(-9.47383654720263,-0.809275815695625,
26.1956185965107));
#33322=CARTESIAN_POINT('Ctrl Pts',(-8.98431418402503,-1.16992509177172,
26.2187725173598));
#33323=CARTESIAN_POINT('Ctrl Pts',(-8.38311423523835,-1.26080241069298,
26.2419264382089));
#33324=CARTESIAN_POINT('Ctrl Pts',(-7.80886688894933,-1.06095235748777,
26.265080359058));
#33325=CARTESIAN_POINT('Ctrl Pts',(-7.39398727066922,-0.616458384095017,
26.2882342799071));
#33326=CARTESIAN_POINT('Ctrl Pts',(-7.23414222788049,-0.0298155056950012,
26.3113882007562));
#33327=CARTESIAN_POINT('Ctrl Pts',(-7.36618999782964,0.563701837361564,
26.3345421216053));
#33328=CARTESIAN_POINT('Ctrl Pts',(-7.75968238765149,1.02723719824325,26.3576960424544));
#33329=CARTESIAN_POINT('Ctrl Pts',(-8.2913615143234,1.24083453904628,26.3795153352526));
#33330=CARTESIAN_POINT('Ctrl Pts',(-8.65756915925267,1.21801623774878,26.3936166544345));
#33331=CARTESIAN_POINT('Ctrl Pts',(-8.81482194563459,1.17607986114086,26.4));
#33332=CARTESIAN_POINT('Origin',(-8.5,0.,24.5374873996035));
#33333=CARTESIAN_POINT('',(-9.71737950437713,-1.72188301428289E-5,25.8625126003965));
#33334=CARTESIAN_POINT('',(-9.71750638855972,-2.14937524795297E-5,25.8874873996035));
#33335=CARTESIAN_POINT('',(-9.71745,-6.10603367124078E-16,24.5374873996035));
#33336=CARTESIAN_POINT('Ctrl Pts',(-9.71750638855971,-2.14937524796385E-5,
25.8874873996035));
#33337=CARTESIAN_POINT('Ctrl Pts',(-9.71752861008525,-0.0265897937602074,
25.888529513509));
#33338=CARTESIAN_POINT('Ctrl Pts',(-9.71035873773204,-0.24991293726262,
25.8972896010309));
#33339=CARTESIAN_POINT('Ctrl Pts',(-9.57920099393642,-0.662276467266634,
25.9137676621692));
#33340=CARTESIAN_POINT('Ctrl Pts',(-9.14605449749695,-1.08898966509019,
25.9369215830183));
#33341=CARTESIAN_POINT('Ctrl Pts',(-8.56393486896201,-1.2645937042741,25.9600755038673));
#33342=CARTESIAN_POINT('Ctrl Pts',(-7.96707255574195,-1.14859620568215,
25.9832294247164));
#33343=CARTESIAN_POINT('Ctrl Pts',(-7.49309750825848,-0.767744929110479,
26.0063833455655));
#33344=CARTESIAN_POINT('Ctrl Pts',(-7.25130321058993,-0.209860032372193,
26.0295372664146));
#33345=CARTESIAN_POINT('Ctrl Pts',(-7.29744479634916,0.396416303503929,
26.0526911872637));
#33346=CARTESIAN_POINT('Ctrl Pts',(-7.62088251501485,0.911283354515532,
26.0758451081128));
#33347=CARTESIAN_POINT('Ctrl Pts',(-8.14703515781832,1.21601839122289,26.0989990289619));
#33348=CARTESIAN_POINT('Ctrl Pts',(-8.75457763896279,1.24035281914371,26.122152949811));
#33349=CARTESIAN_POINT('Ctrl Pts',(-9.30341731233995,0.978675413103695,
26.14530687066));
#33350=CARTESIAN_POINT('Ctrl Pts',(-9.64539425734869,0.520283629650974,
26.1670850205909));
#33351=CARTESIAN_POINT('Ctrl Pts',(-9.71733342562011,0.16167563114474,26.1811451969054));
#33352=CARTESIAN_POINT('Ctrl Pts',(-9.71748325610114,-2.53302756962961E-5,
26.1874873996035));
#33353=CARTESIAN_POINT('Ctrl Pts',(-9.71737950437712,-1.72188301428705E-5,
25.8625126003965));
#33354=CARTESIAN_POINT('Ctrl Pts',(-9.71741998136212,-0.0761084197418133,
25.8654963018055));
#33355=CARTESIAN_POINT('Ctrl Pts',(-9.69220323214041,-0.348999073966435,
25.8761979768309));
#33356=CARTESIAN_POINT('Ctrl Pts',(-9.49058720348329,-0.788683685422225,
25.8946176254726));
#33357=CARTESIAN_POINT('Ctrl Pts',(-9.00873260835677,-1.15951545765943,
25.9177715463217));
#33358=CARTESIAN_POINT('Ctrl Pts',(-8.40956981340752,-1.26297559149317,
25.9409254671708));
#33359=CARTESIAN_POINT('Ctrl Pts',(-7.83125923477822,-1.07520730665756,
25.9640793880199));
#33360=CARTESIAN_POINT('Ctrl Pts',(-7.40715299459429,-0.63950792499141,
25.987233308869));
#33361=CARTESIAN_POINT('Ctrl Pts',(-7.2350453736822,-0.056344979529684,
26.0103872297181));
#33362=CARTESIAN_POINT('Ctrl Pts',(-7.35462251532982,0.539810504688725,
26.0335411505671));
#33363=CARTESIAN_POINT('Ctrl Pts',(-7.73831123274286,1.0114915645451,26.0566950714162));
#33364=CARTESIAN_POINT('Ctrl Pts',(-8.29763708577969,1.24993368402129,26.0798489922653));
#33365=CARTESIAN_POINT('Ctrl Pts',(-8.90362562319939,1.20015470640273,26.1030029131144));
#33366=CARTESIAN_POINT('Ctrl Pts',(-9.41654248721522,0.873633122741245,
26.1261568339635));
#33367=CARTESIAN_POINT('Ctrl Pts',(-9.67490713951847,0.421305975808577,
26.1459933963908));
#33368=CARTESIAN_POINT('Ctrl Pts',(-9.7173298280956,0.112217608765634,26.1581119852019));
#33369=CARTESIAN_POINT('Ctrl Pts',(-9.71736802727299,-1.11661151495218E-5,
26.1625126003965));
#33370=CARTESIAN_POINT('Origin',(-8.5,0.,24.5374873996035));
#33371=CARTESIAN_POINT('',(-9.71739568233103,-2.21443141968369E-5,25.5625126003965));
#33372=CARTESIAN_POINT('',(-9.7175261349988,-1.58793738679787E-5,25.5874873996035));
#33373=CARTESIAN_POINT('',(-9.71745,-6.10603367124078E-16,24.5374873996035));
#33374=CARTESIAN_POINT('Ctrl Pts',(-9.7175261349988,-1.58793738680163E-5,
25.5874873996035));
#33375=CARTESIAN_POINT('Ctrl Pts',(-9.71753816754102,-0.0180768701490775,
25.5881958564963));
#33376=CARTESIAN_POINT('Ctrl Pts',(-9.71285149565645,-0.232889174626129,
25.5966222870055));
#33377=CARTESIAN_POINT('Ctrl Pts',(-9.59284698531382,-0.639507913234122,
25.612766691131));
#33378=CARTESIAN_POINT('Ctrl Pts',(-9.16874075292704,-1.07520728689,25.6359206119801));
#33379=CARTESIAN_POINT('Ctrl Pts',(-8.59043018492992,-1.26297556827349,
25.6590745328292));
#33380=CARTESIAN_POINT('Ctrl Pts',(-7.99126740099621,-1.15951543634185,
25.6822284536783));
#33381=CARTESIAN_POINT('Ctrl Pts',(-7.50941281472855,-0.788683670922342,
25.7053823745274));
#33382=CARTESIAN_POINT('Ctrl Pts',(-7.25597684673547,-0.235990039080846,
25.7285362953765));
#33383=CARTESIAN_POINT('Ctrl Pts',(-7.28939907153445,0.371120326042741,
25.7516902162256));
#33384=CARTESIAN_POINT('Ctrl Pts',(-7.60197268802659,0.892654385164513,
25.7748441370747));
#33385=CARTESIAN_POINT('Ctrl Pts',(-8.12162162390845,1.2083520633118,25.7979980579237));
#33386=CARTESIAN_POINT('Ctrl Pts',(-8.7285204930998,1.2454169135826,25.8211519787728));
#33387=CARTESIAN_POINT('Ctrl Pts',(-9.2827250249746,0.995302185107979,25.8443058996219));
#33388=CARTESIAN_POINT('Ctrl Pts',(-9.63962141358243,0.537268419868294,
25.8664177065655));
#33389=CARTESIAN_POINT('Ctrl Pts',(-9.7173640358032,0.170177025493677,25.8808115398927));
#33390=CARTESIAN_POINT('Ctrl Pts',(-9.71750638855971,-2.14937524796385E-5,
25.8874873996035));
#33391=CARTESIAN_POINT('Ctrl Pts',(-9.71739568233103,-2.2144314196941E-5,
25.5625126003965));
#33392=CARTESIAN_POINT('Ctrl Pts',(-9.71744285456702,-0.0676017501666064,
25.5651626447928));
#33393=CARTESIAN_POINT('Ctrl Pts',(-9.69577288570607,-0.331969861171505,
25.5755306628055));
#33394=CARTESIAN_POINT('Ctrl Pts',(-9.50690251025353,-0.767744943225855,
25.5936166544345));
#33395=CARTESIAN_POINT('Ctrl Pts',(-9.03292745405576,-1.14859622679878,
25.6167705752836));
#33396=CARTESIAN_POINT('Ctrl Pts',(-8.4360651298626,-1.26459372752363,25.6399244961327));
#33397=CARTESIAN_POINT('Ctrl Pts',(-7.85394549062537,-1.08898968511111,
25.6630784169818));
#33398=CARTESIAN_POINT('Ctrl Pts',(-7.42079898622258,-0.662276479442534,
25.6862323378308));
#33399=CARTESIAN_POINT('Ctrl Pts',(-7.23650448403929,-0.0828495292575919,
25.7093862586799));
#33400=CARTESIAN_POINT('Ctrl Pts',(-7.34355828943908,0.515681620221391,
25.732540179529));
#33401=CARTESIAN_POINT('Ctrl Pts',(-7.71727496063508,0.995302203406518,
25.7556941003781));
#33402=CARTESIAN_POINT('Ctrl Pts',(-8.27147950269888,1.24541693647946,25.7788480212272));
#33403=CARTESIAN_POINT('Ctrl Pts',(-8.878378383048,1.20835208552723,25.8020019420763));
#33404=CARTESIAN_POINT('Ctrl Pts',(-9.39802732848356,0.892654401575867,
25.8251558629253));
#33405=CARTESIAN_POINT('Ctrl Pts',(-9.67032153700355,0.43832717639768,25.8453260823654));
#33406=CARTESIAN_POINT('Ctrl Pts',(-9.71731527909489,0.120717535865137,
25.8577783281891));
#33407=CARTESIAN_POINT('Ctrl Pts',(-9.71737950437712,-1.72188301428705E-5,
25.8625126003965));
#33408=CARTESIAN_POINT('Origin',(-8.5,0.,24.5374873996035));
#33409=CARTESIAN_POINT('',(-9.71741565872953,-3.18308007817847E-5,25.2625126003965));
#33410=CARTESIAN_POINT('',(-9.7175402933437,-8.82488467109868E-6,25.2874873996035));
#33411=CARTESIAN_POINT('',(-9.71745,-6.10603367124078E-16,24.5374873996035));
#33412=CARTESIAN_POINT('',(-8.81478889550441,1.17604951161383,25.2));
#33413=CARTESIAN_POINT('Ctrl Pts',(-8.8147888955044,1.17604951161383,25.2));
#33414=CARTESIAN_POINT('Ctrl Pts',(-9.00489125583826,1.12516550422186,25.2077179736164));
#33415=CARTESIAN_POINT('Ctrl Pts',(-9.35978529202387,0.929507318017654,
25.2231539208491));
#33416=CARTESIAN_POINT('Ctrl Pts',(-9.66055721233611,0.472338081655336,
25.2439914543146));
#33417=CARTESIAN_POINT('Ctrl Pts',(-9.71730344186206,0.137705854269909,
25.2571110141637));
#33418=CARTESIAN_POINT('Ctrl Pts',(-9.71741565872953,-3.18308007818402E-5,
25.2625126003965));
#33419=CARTESIAN_POINT('',(-8.18517804880579,1.17607982959759,25.2));
#33420=CARTESIAN_POINT('Origin',(-8.5,0.,25.2));
#33421=CARTESIAN_POINT('Ctrl Pts',(-8.18517804880579,1.17607982959759,25.2));
#33422=CARTESIAN_POINT('Ctrl Pts',(-8.3424308355762,1.21801620838825,25.2063833455655));
#33423=CARTESIAN_POINT('Ctrl Pts',(-8.70863847539721,1.24083450908453,25.2204846647474));
#33424=CARTESIAN_POINT('Ctrl Pts',(-9.24031759749596,1.02723717888941,25.2423039575457));
#33425=CARTESIAN_POINT('Ctrl Pts',(-9.62744039394288,0.571205219807404,
25.2650830785146));
#33426=CARTESIAN_POINT('Ctrl Pts',(-9.71746406825214,0.187187424104769,
25.2801442258672));
#33427=CARTESIAN_POINT('Ctrl Pts',(-9.71754029334369,-8.82488467114119E-6,
25.2874873996035));
#33428=CARTESIAN_POINT('Origin',(-8.5,0.,24.5374873996035));
#33429=CARTESIAN_POINT('Ctrl Pts',(-9.71754029334369,-8.82488467114119E-6,
25.2874873996035));
#33430=CARTESIAN_POINT('Ctrl Pts',(-9.71754418391693,-0.00956343086266385,
25.2878621994836));
#33431=CARTESIAN_POINT('Ctrl Pts',(-9.71516353125157,-0.215866953049769,
25.2959549729801));
#33432=CARTESIAN_POINT('Ctrl Pts',(-9.60601270884069,-0.616458373015401,
25.3117657200929));
#33433=CARTESIAN_POINT('Ctrl Pts',(-9.19113309833576,-1.06095233793524,
25.334919640942));
#33434=CARTESIAN_POINT('Ctrl Pts',(-8.61688576258933,-1.26080238756323,
25.3580735617911));
#33435=CARTESIAN_POINT('Ctrl Pts',(-8.01568582487961,-1.16992507024812,
25.3812274826402));
#33436=CARTESIAN_POINT('Ctrl Pts',(-7.52616347069768,-0.809275800827533,
25.4043814034893));
#33437=CARTESIAN_POINT('Ctrl Pts',(-7.26119721213712,-0.262016330420185,
25.4275353243383));
#33438=CARTESIAN_POINT('Ctrl Pts',(-7.28188538871804,0.345661246443408,
25.4506892451874));
#33439=CARTESIAN_POINT('Ctrl Pts',(-7.58345752963543,0.873633106680533,
25.4738431660365));
#33440=CARTESIAN_POINT('Ctrl Pts',(-8.09637438422115,1.20015468433752,25.4969970868856));
#33441=CARTESIAN_POINT('Ctrl Pts',(-8.70236291049992,1.2499336610416,25.5201510077347));
#33442=CARTESIAN_POINT('Ctrl Pts',(-9.26168875325356,1.01149154594881,25.5433049285838));
#33443=CARTESIAN_POINT('Ctrl Pts',(-9.63363746876147,0.554242853504049,
25.56575039254));
#33444=CARTESIAN_POINT('Ctrl Pts',(-9.71740708427495,0.178680690828068,
25.58047788288));
#33445=CARTESIAN_POINT('Ctrl Pts',(-9.7175261349988,-1.58793738680163E-5,
25.5874873996035));
#33446=CARTESIAN_POINT('Ctrl Pts',(-9.71741565872953,-3.18308007818402E-5,
25.2625126003965));
#33447=CARTESIAN_POINT('Ctrl Pts',(-9.71746378121149,-0.0590985238410443,
25.2648289877801));
#33448=CARTESIAN_POINT('Ctrl Pts',(-9.6991494544252,-0.314940022053408,
25.27486334878));
#33449=CARTESIAN_POINT('Ctrl Pts',(-9.52277787696657,-0.746472135969,25.2926156833964));
#33450=CARTESIAN_POINT('Ctrl Pts',(-9.05688673586305,-1.13717144686837,
25.3157696042454));
#33451=CARTESIAN_POINT('Ctrl Pts',(-8.46258910686823,-1.26565668871267,
25.3389235250945));
#33452=CARTESIAN_POINT('Ctrl Pts',(-7.87691540315674,-1.10229327660247,
25.3620774459436));
#33453=CARTESIAN_POINT('Ctrl Pts',(-7.43491939071853,-0.684754086769719,
25.3852313667927));
#33454=CARTESIAN_POINT('Ctrl Pts',(-7.23851882542848,-0.109317624216872,
25.4083852876418));
#33455=CARTESIAN_POINT('Ctrl Pts',(-7.3330023279845,0.49132607864821,25.4315392084909));
#33456=CARTESIAN_POINT('Ctrl Pts',(-7.69658267289797,0.978675431042071,
25.45469312934));
#33457=CARTESIAN_POINT('Ctrl Pts',(-8.24542235634912,1.24035284195992,25.477847050189));
#33458=CARTESIAN_POINT('Ctrl Pts',(-8.85296484867377,1.21601841356867,25.5010009710381));
#33459=CARTESIAN_POINT('Ctrl Pts',(-9.37911750114581,0.911283371272776,
25.5241548918872));
#33460=CARTESIAN_POINT('Ctrl Pts',(-9.66553668642746,0.455344583774923,
25.54465876834));
#33461=CARTESIAN_POINT('Ctrl Pts',(-9.7173054704261,0.129216693970434,25.5574446711764));
#33462=CARTESIAN_POINT('Ctrl Pts',(-9.71739568233103,-2.2144314196941E-5,
25.5625126003965));
#33463=CARTESIAN_POINT('Ctrl Pts',(-7.70661869325989,-0.687936125025681,
25.2));
#33464=CARTESIAN_POINT('Ctrl Pts',(-7.59541735366079,-0.559690113640417,
25.2077179736164));
#33465=CARTESIAN_POINT('Ctrl Pts',(-7.43648251267377,-0.248363425571168,
25.2231539208491));
#33466=CARTESIAN_POINT('Ctrl Pts',(-7.44330961637993,0.276076624849719,
25.2463078416982));
#33467=CARTESIAN_POINT('Ctrl Pts',(-7.69382613010723,0.736801382201653,
25.2694617625473));
#33468=CARTESIAN_POINT('Ctrl Pts',(-8.13023254087597,1.02766020195344,25.2926156833963));
#33469=CARTESIAN_POINT('Ctrl Pts',(-8.65190812324789,1.08153933511494,25.3157696042454));
#33470=CARTESIAN_POINT('Ctrl Pts',(-9.13855395222022,0.886033727505665,
25.3389235250945));
#33471=CARTESIAN_POINT('Ctrl Pts',(-9.47795709088013,0.48621568614451,25.3620774459436));
#33472=CARTESIAN_POINT('Ctrl Pts',(-9.59185364649637,-0.0257170823187401,
25.3852313667927));
#33473=CARTESIAN_POINT('Ctrl Pts',(-9.45398081691536,-0.53172034786108,
25.4083852876418));
#33474=CARTESIAN_POINT('Ctrl Pts',(-9.09613032696405,-0.915114419537387,
25.4315392084909));
#33475=CARTESIAN_POINT('Ctrl Pts',(-8.60081871066168,-1.0874931924762,25.45469312934));
#33476=CARTESIAN_POINT('Ctrl Pts',(-8.08225938207407,-1.00910782066413,
25.4778470501891));
#33477=CARTESIAN_POINT('Ctrl Pts',(-7.66002649848424,-0.698033199268136,
25.5010009710381));
#33478=CARTESIAN_POINT('Ctrl Pts',(-7.43148235448289,-0.225999711342754,
25.5241548918872));
#33479=CARTESIAN_POINT('Ctrl Pts',(-7.44932674581528,0.298146843722718,
25.5473088127363));
#33480=CARTESIAN_POINT('Ctrl Pts',(-7.7094449479405,0.753543985646414,25.5704627335854));
#33481=CARTESIAN_POINT('Ctrl Pts',(-8.15185653691784,1.0351820888109,25.5936166544345));
#33482=CARTESIAN_POINT('Ctrl Pts',(-8.67454621735263,1.07811847505834,25.6167705752836));
#33483=CARTESIAN_POINT('Ctrl Pts',(-9.15698744079146,0.872452480513238,
25.6399244961327));
#33484=CARTESIAN_POINT('Ctrl Pts',(-9.48793451438624,0.465608444332083,
25.6630784169817));
#33485=CARTESIAN_POINT('Ctrl Pts',(-9.59107464674124,-0.048599829082402,
25.6862323378308));
#33486=CARTESIAN_POINT('Ctrl Pts',(-9.44262484642329,-0.551601511098732,
25.7093862586799));
#33487=CARTESIAN_POINT('Ctrl Pts',(-9.07681602090327,-0.927409891135722,
25.732540179529));
#33488=CARTESIAN_POINT('Ctrl Pts',(-8.5779997019959,-1.08936764897449,25.7556941003781));
#33489=CARTESIAN_POINT('Ctrl Pts',(-8.06119750115908,-1.00012908924603,
25.7788480212272));
#33490=CARTESIAN_POINT('Ctrl Pts',(-7.64557837836991,-0.680271652088834,
25.8020019420763));
#33491=CARTESIAN_POINT('Ctrl Pts',(-7.4269795776064,-0.203550979538212,
25.8251558629254));
#33492=CARTESIAN_POINT('Ctrl Pts',(-7.45580760196995,0.32010633239762,25.8483097837744));
#33493=CARTESIAN_POINT('Ctrl Pts',(-7.72541502295513,0.769950609767346,
25.8714637046235));
#33494=CARTESIAN_POINT('Ctrl Pts',(-8.17363330507722,1.04225266062977,25.8946176254726));
#33495=CARTESIAN_POINT('Ctrl Pts',(-8.69710819319406,1.07422259719338,25.9177715463217));
#33496=CARTESIAN_POINT('Ctrl Pts',(-9.17513207829958,0.858488500211005,
25.9409254671708));
#33497=CARTESIAN_POINT('Ctrl Pts',(-9.49747785776318,0.444796303288628,
25.9640793880199));
#33498=CARTESIAN_POINT('Ctrl Pts',(-9.58981610490559,-0.0714610777230468,
25.987233308869));
#33499=CARTESIAN_POINT('Ctrl Pts',(-9.43085462543237,-0.57124031235508,
26.0103872297181));
#33500=CARTESIAN_POINT('Ctrl Pts',(-9.05724820552922,-0.939297751292626,
26.0335411505671));
#33501=CARTESIAN_POINT('Ctrl Pts',(-8.55514641742741,-1.09076335690027,
26.0566950714162));
#33502=CARTESIAN_POINT('Ctrl Pts',(-8.04032846587919,-0.990710809960839,
26.0798489922653));
#33503=CARTESIAN_POINT('Ctrl Pts',(-7.6315057648546,-0.662211138082807,
26.1030029131144));
#33504=CARTESIAN_POINT('Ctrl Pts',(-7.42294837688651,-0.181012789021348,
26.1261568339635));
#33505=CARTESIAN_POINT('Ctrl Pts',(-7.46274736592571,0.341925138863589,
26.1493107548126));
#33506=CARTESIAN_POINT('Ctrl Pts',(-7.74172551564097,0.786018851350577,
26.1724646756617));
#33507=CARTESIAN_POINT('Ctrl Pts',(-8.19555350874781,1.0488651793693,26.1956185965107));
#33508=CARTESIAN_POINT('Ctrl Pts',(-8.71958353827659,1.06985461036002,26.2187725173598));
#33509=CARTESIAN_POINT('Ctrl Pts',(-9.19298001535027,0.844147235040609,
26.2419264382089));
#33510=CARTESIAN_POINT('Ctrl Pts',(-9.50658280242999,0.423788661273173,
26.265080359058));
#33511=CARTESIAN_POINT('Ctrl Pts',(-9.58807865380676,-0.0942908823910285,
26.2882342799071));
#33512=CARTESIAN_POINT('Ctrl Pts',(-9.41867520397754,-0.590628159917251,
26.3113882007562));
#33513=CARTESIAN_POINT('Ctrl Pts',(-9.03743572467889,-0.95077263680366,
26.3345421216053));
#33514=CARTESIAN_POINT('Ctrl Pts',(-8.53226841131125,-1.0916802030838,26.3576960424544));
#33515=CARTESIAN_POINT('Ctrl Pts',(-8.01966261282913,-0.980856465439986,
26.3808499633034));
#33516=CARTESIAN_POINT('Ctrl Pts',(-7.61781261410204,-0.643862470306016,
26.4040038841525));
#33517=CARTESIAN_POINT('Ctrl Pts',(-7.41939638262019,-0.158393205087297,
26.4271578050016));
#33518=CARTESIAN_POINT('Ctrl Pts',(-7.47013324212837,0.363575756417424,
26.4503117258507));
#33519=CARTESIAN_POINT('Ctrl Pts',(-7.75840028659244,0.801737926060614,
26.4734656466998));
#33520=CARTESIAN_POINT('Ctrl Pts',(-8.06451081542917,0.970500879693931,
26.4889015939325));
#33521=CARTESIAN_POINT('Ctrl Pts',(-8.22848181102372,1.01439039972539,26.4966195675489));
#33522=CARTESIAN_POINT('Ctrl Pts',(-7.66447275106931,-0.72448061619257,
25.1677934774837));
#33523=CARTESIAN_POINT('Ctrl Pts',(-7.5473641822597,-0.58942192982228,25.1755114511001));
#33524=CARTESIAN_POINT('Ctrl Pts',(-7.3799864165864,-0.261556968811283,
25.1909473983328));
#33525=CARTESIAN_POINT('Ctrl Pts',(-7.3871761891829,0.290742346580538,25.2141013191819));
#33526=CARTESIAN_POINT('Ctrl Pts',(-7.65100062233763,0.77594168989027,25.237255240031));
#33527=CARTESIAN_POINT('Ctrl Pts',(-8.11058978168339,1.08225149002027,25.2604091608801));
#33528=CARTESIAN_POINT('Ctrl Pts',(-8.65997777516216,1.13899278644703,25.2835630817291));
#33529=CARTESIAN_POINT('Ctrl Pts',(-9.17247516731213,0.933101544633581,
25.3067170025782));
#33530=CARTESIAN_POINT('Ctrl Pts',(-9.52990805401342,0.512044399307156,
25.3298709234273));
#33531=CARTESIAN_POINT('Ctrl Pts',(-9.64985501390302,-0.0270832232342217,
25.3530248442764));
#33532=CARTESIAN_POINT('Ctrl Pts',(-9.5046581142238,-0.559966356245853,
25.3761787651255));
#33533=CARTESIAN_POINT('Ctrl Pts',(-9.12779791742128,-0.963727059003338,
25.3993326859746));
#33534=CARTESIAN_POINT('Ctrl Pts',(-8.60617439463756,-1.14526292417188,
25.4224866068237));
#33535=CARTESIAN_POINT('Ctrl Pts',(-8.06006819634258,-1.06271357052546,
25.4456405276728));
#33536=CARTESIAN_POINT('Ctrl Pts',(-7.61540548922205,-0.735114066454602,
25.4687944485218));
#33537=CARTESIAN_POINT('Ctrl Pts',(-7.37472064036763,-0.238005251035231,
25.4919483693709));
#33538=CARTESIAN_POINT('Ctrl Pts',(-7.3935129601162,0.313984977962948,25.51510229022));
#33539=CARTESIAN_POINT('Ctrl Pts',(-7.66744914183881,0.793573692657787,
25.5382562110691));
#33540=CARTESIAN_POINT('Ctrl Pts',(-8.13336248601895,1.09017295398644,25.5614101319182));
#33541=CARTESIAN_POINT('Ctrl Pts',(-8.68381844840173,1.13539020371943,25.5845640527673));
#33542=CARTESIAN_POINT('Ctrl Pts',(-9.19188787827883,0.918798835658428,
25.6077179736164));
#33543=CARTESIAN_POINT('Ctrl Pts',(-9.54041549746167,0.490342461142855,
25.6308718944655));
#33544=CARTESIAN_POINT('Ctrl Pts',(-9.6490346321814,-0.0511815455528781,
25.6540258153145));
#33545=CARTESIAN_POINT('Ctrl Pts',(-9.49269889272013,-0.580903645143862,
25.6771797361636));
#33546=CARTESIAN_POINT('Ctrl Pts',(-9.10745759824453,-0.97667568972048,
25.7003336570127));
#33547=CARTESIAN_POINT('Ctrl Pts',(-8.58214319630724,-1.14723695540749,
25.7234875778618));
#33548=CARTESIAN_POINT('Ctrl Pts',(-8.03788746777146,-1.0532578716113,25.7466414987109));
#33549=CARTESIAN_POINT('Ctrl Pts',(-7.60018985715613,-0.716408991700003,
25.76979541956));
#33550=CARTESIAN_POINT('Ctrl Pts',(-7.36997866731609,-0.214363999385756,
25.7929493404091));
#33551=CARTESIAN_POINT('Ctrl Pts',(-7.40033809182479,0.337110996945993,
25.8161032612581));
#33552=CARTESIAN_POINT('Ctrl Pts',(-7.68426757797895,0.810851868233069,
25.8392571821072));
#33553=CARTESIAN_POINT('Ctrl Pts',(-8.15629607802097,1.09761912819045,25.8624111029563));
#33554=CARTESIAN_POINT('Ctrl Pts',(-8.7075789598293,1.13128736932312,25.8855650238054));
#33555=CARTESIAN_POINT('Ctrl Pts',(-9.21099639385792,0.904093061843329,
25.9087189446545));
#33556=CARTESIAN_POINT('Ctrl Pts',(-9.55046580160874,0.468424739105964,
25.9318728655036));
#33557=CARTESIAN_POINT('Ctrl Pts',(-9.64770923418088,-0.0752572277268409,
25.9550267863527));
#33558=CARTESIAN_POINT('Ctrl Pts',(-9.48030341493372,-0.601585697325598,
25.9781807072018));
#33559=CARTESIAN_POINT('Ctrl Pts',(-9.08685030285179,-0.989195055891815,
26.0013346280508));
#33560=CARTESIAN_POINT('Ctrl Pts',(-8.55807590127228,-1.14870680602488,
26.0244885488999));
#33561=CARTESIAN_POINT('Ctrl Pts',(-8.01590982916678,-1.04333927520127,
26.047642469749));
#33562=CARTESIAN_POINT('Ctrl Pts',(-7.58536967932256,-0.697389068425364,
26.0707963905981));
#33563=CARTESIAN_POINT('Ctrl Pts',(-7.36573332145432,-0.190628536804963,
26.0939503114472));
#33564=CARTESIAN_POINT('Ctrl Pts',(-7.40764650940019,0.360088860410369,
26.1171042322963));
#33565=CARTESIAN_POINT('Ctrl Pts',(-7.70144451543227,0.827773685738895,
26.1402581531454));
#33566=CARTESIAN_POINT('Ctrl Pts',(-8.17938072510464,1.10458291665383,26.1634120739944));
#33567=CARTESIAN_POINT('Ctrl Pts',(-8.73124823850532,1.12668734662125,26.1865659948435));
#33568=CARTESIAN_POINT('Ctrl Pts',(-9.22979244768016,0.888989961061638,
26.2097199156926));
#33569=CARTESIAN_POINT('Ctrl Pts',(-9.56005441846232,0.44630113070912,26.2328738365417));
#33570=CARTESIAN_POINT('Ctrl Pts',(-9.64587948633527,-0.0992997955637866,
26.2560277573908));
#33571=CARTESIAN_POINT('Ctrl Pts',(-9.46747699916709,-0.622003464669862,
26.2791816782399));
#33572=CARTESIAN_POINT('Ctrl Pts',(-9.06598534488173,-1.00127950940916,
26.302335599089));
#33573=CARTESIAN_POINT('Ctrl Pts',(-8.53398257143344,-1.14967235684252,
26.3254895199381));
#33574=CARTESIAN_POINT('Ctrl Pts',(-7.99414616622307,-1.03296144893089,
26.3486434407871));
#33575=CARTESIAN_POINT('Ctrl Pts',(-7.57094912204414,-0.678065684096992,
26.3717973616362));
#33576=CARTESIAN_POINT('Ctrl Pts',(-7.36199263841535,-0.166807357031988,
26.3949512824853));
#33577=CARTESIAN_POINT('Ctrl Pts',(-7.41542473756378,0.382889600443852,
26.4181052033344));
#33578=CARTESIAN_POINT('Ctrl Pts',(-7.71900508231388,0.844327787955114,
26.4412591241835));
#33579=CARTESIAN_POINT('Ctrl Pts',(-8.04137679167336,1.02205575453657,26.4566950714162));
#33580=CARTESIAN_POINT('Ctrl Pts',(-8.21405824218102,1.06827677035487,26.4644130450326));
#33581=CARTESIAN_POINT('Ctrl Pts',(-7.62232680887874,-0.761025107359458,
25.1355869549674));
#33582=CARTESIAN_POINT('Ctrl Pts',(-7.49931101085861,-0.619153746004144,
25.1433049285838));
#33583=CARTESIAN_POINT('Ctrl Pts',(-7.32349032049903,-0.274750512051398,
25.1587408758165));
#33584=CARTESIAN_POINT('Ctrl Pts',(-7.33104276198587,0.305408068311358,
25.1818947966656));
#33585=CARTESIAN_POINT('Ctrl Pts',(-7.60817511456803,0.815081997578886,
25.2050487175147));
#33586=CARTESIAN_POINT('Ctrl Pts',(-8.0909470224908,1.13684277808709,25.2282026383638));
#33587=CARTESIAN_POINT('Ctrl Pts',(-8.66804742707643,1.19644623777912,25.2513565592129));
#33588=CARTESIAN_POINT('Ctrl Pts',(-9.20639638240405,0.980169361761496,
25.2745104800619));
#33589=CARTESIAN_POINT('Ctrl Pts',(-9.5818590171467,0.537873112469803,25.297664400911));
#33590=CARTESIAN_POINT('Ctrl Pts',(-9.70785638130967,-0.0284493641497029,
25.3208183217601));
#33591=CARTESIAN_POINT('Ctrl Pts',(-9.55533541153225,-0.588212364630628,
25.3439722426092));
#33592=CARTESIAN_POINT('Ctrl Pts',(-9.15946550787852,-1.01233969846929,
25.3671261634583));
#33593=CARTESIAN_POINT('Ctrl Pts',(-8.61153007861345,-1.20303265586756,
25.3902800843074));
#33594=CARTESIAN_POINT('Ctrl Pts',(-8.03787701061109,-1.11631932038679,
25.4134340051565));
#33595=CARTESIAN_POINT('Ctrl Pts',(-7.57078447995986,-0.772194933641068,
25.4365879260056));
#33596=CARTESIAN_POINT('Ctrl Pts',(-7.31795892625238,-0.250010790727708,
25.4597418468546));
#33597=CARTESIAN_POINT('Ctrl Pts',(-7.33769917441712,0.329823112203178,
25.4828957677037));
#33598=CARTESIAN_POINT('Ctrl Pts',(-7.62545333573712,0.833603399669161,
25.5060496885528));
#33599=CARTESIAN_POINT('Ctrl Pts',(-8.11486843512004,1.14516381916198,25.5292036094019));
#33600=CARTESIAN_POINT('Ctrl Pts',(-8.69309067945083,1.19266193238051,25.552357530251));
#33601=CARTESIAN_POINT('Ctrl Pts',(-9.22678831576619,0.965145190803617,
25.5755114511001));
#33602=CARTESIAN_POINT('Ctrl Pts',(-9.59289648053711,0.515076477953626,
25.5986653719492));
#33603=CARTESIAN_POINT('Ctrl Pts',(-9.70699461762157,-0.0537632620233534,
25.6218192927982));
#33604=CARTESIAN_POINT('Ctrl Pts',(-9.54277293901697,-0.610205779188992,
25.6449732136473));
#33605=CARTESIAN_POINT('Ctrl Pts',(-9.13809917558578,-1.02594148830524,
25.6681271344964));
#33606=CARTESIAN_POINT('Ctrl Pts',(-8.58628669061858,-1.20510626184049,
25.6912810553455));
#33607=CARTESIAN_POINT('Ctrl Pts',(-8.01457743438384,-1.10638665397658,
25.7144349761946));
#33608=CARTESIAN_POINT('Ctrl Pts',(-7.55480133594234,-0.752546331311173,
25.7375888970437));
#33609=CARTESIAN_POINT('Ctrl Pts',(-7.31297775702578,-0.225177019233301,
25.7607428178928));
#33610=CARTESIAN_POINT('Ctrl Pts',(-7.34486858167961,0.354115661494367,
25.7838967387419));
#33611=CARTESIAN_POINT('Ctrl Pts',(-7.64312013300277,0.851753126698791,
25.8070506595909));
#33612=CARTESIAN_POINT('Ctrl Pts',(-8.13895885096471,1.15298559575112,25.83020458044));
#33613=CARTESIAN_POINT('Ctrl Pts',(-8.71804972646455,1.18835214145286,25.8533585012891));
#33614=CARTESIAN_POINT('Ctrl Pts',(-9.24686070941626,0.949697623475654,
25.8765124221382));
#33615=CARTESIAN_POINT('Ctrl Pts',(-9.6034537454543,0.4920531749233,25.8996663429873));
#33616=CARTESIAN_POINT('Ctrl Pts',(-9.70560236345618,-0.0790533777306346,
25.9228202638364));
#33617=CARTESIAN_POINT('Ctrl Pts',(-9.52975220443507,-0.631931082296116,
25.9459741846855));
#33618=CARTESIAN_POINT('Ctrl Pts',(-9.11645240017437,-1.039092360491,25.9691281055346));
#33619=CARTESIAN_POINT('Ctrl Pts',(-8.56100538511715,-1.20665025514949,
25.9922820263836));
#33620=CARTESIAN_POINT('Ctrl Pts',(-7.99149119245436,-1.09596774044171,
26.0154359472327));
#33621=CARTESIAN_POINT('Ctrl Pts',(-7.53923359379052,-0.732566998767922,
26.0385898680818));
#33622=CARTESIAN_POINT('Ctrl Pts',(-7.30851826602212,-0.200244284588578,
26.0617437889309));
#33623=CARTESIAN_POINT('Ctrl Pts',(-7.35254565287468,0.378252581957149,
26.08489770978));
#33624=CARTESIAN_POINT('Ctrl Pts',(-7.66116351522356,0.869528520127214,
26.1080516306291));
#33625=CARTESIAN_POINT('Ctrl Pts',(-8.16320794146148,1.16030065393836,26.1312055514782));
#33626=CARTESIAN_POINT('Ctrl Pts',(-8.74291293873406,1.18352008288248,26.1543594723273));
#33627=CARTESIAN_POINT('Ctrl Pts',(-9.26660488001006,0.933832687082666,
26.1775133931763));
#33628=CARTESIAN_POINT('Ctrl Pts',(-9.61352603449465,0.468813600145068,
26.2006673140254));
#33629=CARTESIAN_POINT('Ctrl Pts',(-9.70368031886378,-0.104308708736543,
26.2238212348745));
#33630=CARTESIAN_POINT('Ctrl Pts',(-9.51627879435664,-0.653378769422475,
26.2469751557236));
#33631=CARTESIAN_POINT('Ctrl Pts',(-9.09453496508457,-1.05178638201465,
26.2701290765727));
#33632=CARTESIAN_POINT('Ctrl Pts',(-8.53569673155563,-1.20766451060123,
26.2932829974218));
#33633=CARTESIAN_POINT('Ctrl Pts',(-7.96862971961702,-1.08506643242179,
26.3164369182709));
#33634=CARTESIAN_POINT('Ctrl Pts',(-7.52408562998623,-0.712268897887968,
26.3395908391199));
#33635=CARTESIAN_POINT('Ctrl Pts',(-7.3045888942105,-0.175221508976678,
26.362744759969));
#33636=CARTESIAN_POINT('Ctrl Pts',(-7.3607162329992,0.40220344447028,26.3858986808181));
#33637=CARTESIAN_POINT('Ctrl Pts',(-7.67960987803532,0.886917649849614,
26.4090526016672));
#33638=CARTESIAN_POINT('Ctrl Pts',(-8.01824276791755,1.07361062937922,26.4244885488999));
#33639=CARTESIAN_POINT('Ctrl Pts',(-8.19963467333831,1.12216314098435,26.4322065225163));
#33640=CARTESIAN_POINT('Ctrl Pts',(-7.58018086668817,-0.797569598526346,
25.1033804324511));
#33641=CARTESIAN_POINT('Ctrl Pts',(-7.45125783945751,-0.648885562186007,
25.1110984060675));
#33642=CARTESIAN_POINT('Ctrl Pts',(-7.26699422441166,-0.287944055291513,
25.1265343533002));
#33643=CARTESIAN_POINT('Ctrl Pts',(-7.27490933478883,0.320073790042177,
25.1496882741493));
#33644=CARTESIAN_POINT('Ctrl Pts',(-7.56534960679844,0.854222305267502,
25.1728421949984));
#33645=CARTESIAN_POINT('Ctrl Pts',(-8.07130426329821,1.19143406615391,25.1959961158475));
#33646=CARTESIAN_POINT('Ctrl Pts',(-8.67611707899071,1.25389968911121,25.2191500366966));
#33647=CARTESIAN_POINT('Ctrl Pts',(-9.24031759749596,1.02723717888941,25.2423039575457));
#33648=CARTESIAN_POINT('Ctrl Pts',(-9.63380998027999,0.563701825632449,
25.2654578783947));
#33649=CARTESIAN_POINT('Ctrl Pts',(-9.76585774871632,-0.0298155050651843,
25.2886117992438));
#33650=CARTESIAN_POINT('Ctrl Pts',(-9.60601270884069,-0.616458373015401,
25.3117657200929));
#33651=CARTESIAN_POINT('Ctrl Pts',(-9.19113309833576,-1.06095233793524,
25.334919640942));
#33652=CARTESIAN_POINT('Ctrl Pts',(-8.61688576258933,-1.26080238756323,
25.3580735617911));
#33653=CARTESIAN_POINT('Ctrl Pts',(-8.01568582487961,-1.16992507024812,
25.3812274826402));
#33654=CARTESIAN_POINT('Ctrl Pts',(-7.52616347069768,-0.809275800827533,
25.4043814034893));
#33655=CARTESIAN_POINT('Ctrl Pts',(-7.26119721213712,-0.262016330420185,
25.4275353243383));
#33656=CARTESIAN_POINT('Ctrl Pts',(-7.28188538871804,0.345661246443408,
25.4506892451874));
#33657=CARTESIAN_POINT('Ctrl Pts',(-7.58345752963543,0.873633106680533,
25.4738431660365));
#33658=CARTESIAN_POINT('Ctrl Pts',(-8.09637438422115,1.20015468433752,25.4969970868856));
#33659=CARTESIAN_POINT('Ctrl Pts',(-8.70236291049992,1.2499336610416,25.5201510077347));
#33660=CARTESIAN_POINT('Ctrl Pts',(-9.26168875325356,1.01149154594881,25.5433049285838));
#33661=CARTESIAN_POINT('Ctrl Pts',(-9.64537746361254,0.539810494764398,
25.5664588494329));
#33662=CARTESIAN_POINT('Ctrl Pts',(-9.76495460306173,-0.0563449784938296,
25.5896127702819));
#33663=CARTESIAN_POINT('Ctrl Pts',(-9.59284698531382,-0.639507913234122,
25.612766691131));
#33664=CARTESIAN_POINT('Ctrl Pts',(-9.16874075292704,-1.07520728689,25.6359206119801));
#33665=CARTESIAN_POINT('Ctrl Pts',(-8.59043018492992,-1.26297556827349,
25.6590745328292));
#33666=CARTESIAN_POINT('Ctrl Pts',(-7.99126740099621,-1.15951543634185,
25.6822284536783));
#33667=CARTESIAN_POINT('Ctrl Pts',(-7.50941281472855,-0.788683670922342,
25.7053823745274));
#33668=CARTESIAN_POINT('Ctrl Pts',(-7.25597684673547,-0.235990039080846,
25.7285362953765));
#33669=CARTESIAN_POINT('Ctrl Pts',(-7.28939907153445,0.371120326042741,
25.7516902162256));
#33670=CARTESIAN_POINT('Ctrl Pts',(-7.60197268802659,0.892654385164513,
25.7748441370747));
#33671=CARTESIAN_POINT('Ctrl Pts',(-8.12162162390845,1.2083520633118,25.7979980579237));
#33672=CARTESIAN_POINT('Ctrl Pts',(-8.7285204930998,1.2454169135826,25.8211519787728));
#33673=CARTESIAN_POINT('Ctrl Pts',(-9.2827250249746,0.995302185107979,25.8443058996219));
#33674=CARTESIAN_POINT('Ctrl Pts',(-9.65644168929986,0.515681610740635,
25.867459820471));
#33675=CARTESIAN_POINT('Ctrl Pts',(-9.76349549273147,-0.0828495277344286,
25.8906137413201));
#33676=CARTESIAN_POINT('Ctrl Pts',(-9.57920099393642,-0.662276467266634,
25.9137676621692));
#33677=CARTESIAN_POINT('Ctrl Pts',(-9.14605449749695,-1.08898966509019,
25.9369215830183));
#33678=CARTESIAN_POINT('Ctrl Pts',(-8.56393486896201,-1.2645937042741,25.9600755038673));
#33679=CARTESIAN_POINT('Ctrl Pts',(-7.96707255574195,-1.14859620568215,
25.9832294247164));
#33680=CARTESIAN_POINT('Ctrl Pts',(-7.49309750825848,-0.767744929110479,
26.0063833455655));
#33681=CARTESIAN_POINT('Ctrl Pts',(-7.25130321058993,-0.209860032372193,
26.0295372664146));
#33682=CARTESIAN_POINT('Ctrl Pts',(-7.29744479634916,0.396416303503929,
26.0526911872637));
#33683=CARTESIAN_POINT('Ctrl Pts',(-7.62088251501485,0.911283354515532,
26.0758451081128));
#33684=CARTESIAN_POINT('Ctrl Pts',(-8.14703515781832,1.21601839122289,26.0989990289619));
#33685=CARTESIAN_POINT('Ctrl Pts',(-8.75457763896279,1.24035281914371,26.122152949811));
#33686=CARTESIAN_POINT('Ctrl Pts',(-9.30341731233995,0.978675413103695,
26.14530687066));
#33687=CARTESIAN_POINT('Ctrl Pts',(-9.66699765052699,0.491326069581015,
26.1684607915091));
#33688=CARTESIAN_POINT('Ctrl Pts',(-9.76148115139229,-0.109317621909302,
26.1916147123582));
#33689=CARTESIAN_POINT('Ctrl Pts',(-9.56508058954619,-0.684754074175086,
26.2147686332073));
#33690=CARTESIAN_POINT('Ctrl Pts',(-9.12308458528742,-1.10229325462015,
26.2379225540564));
#33691=CARTESIAN_POINT('Ctrl Pts',(-8.53741089167782,-1.26565666435994,
26.2610764749055));
#33692=CARTESIAN_POINT('Ctrl Pts',(-7.94311327301097,-1.13717141591269,
26.2842303957546));
#33693=CARTESIAN_POINT('Ctrl Pts',(-7.47722213792833,-0.746472111678944,
26.3073843166037));
#33694=CARTESIAN_POINT('Ctrl Pts',(-7.24718515000566,-0.183635660921369,
26.3305382374527));
#33695=CARTESIAN_POINT('Ctrl Pts',(-7.30600772843461,0.421517288496708,
26.3536921583018));
#33696=CARTESIAN_POINT('Ctrl Pts',(-7.64021467375676,0.929507511744114,
26.3768460791509));
#33697=CARTESIAN_POINT('Ctrl Pts',(-7.99510874416174,1.12516550422186,26.3922820263836));
#33698=CARTESIAN_POINT('Ctrl Pts',(-8.1852111044956,1.17604951161383,26.4));
#33699=CARTESIAN_POINT('Ctrl Pts',(-8.1852111044956,1.17604951161383,26.4));
#33700=CARTESIAN_POINT('Ctrl Pts',(-8.13719978503581,1.15963878614564,26.4));
#33701=CARTESIAN_POINT('Ctrl Pts',(-8.09039266389787,1.14022121612444,26.4));
#33702=CARTESIAN_POINT('Ctrl Pts',(-8.045027575811,1.1179877975994,26.4));
#33703=CARTESIAN_POINT('Ctrl Pts',(-7.99968396671727,1.09576490592363,26.4));
#33704=CARTESIAN_POINT('Ctrl Pts',(-7.95578012736231,1.07072813106631,26.4));
#33705=CARTESIAN_POINT('Ctrl Pts',(-7.91358079345595,1.04302395957461,26.4));
#33706=CARTESIAN_POINT('Ctrl Pts',(-7.87480205233853,1.01756543227811,26.4));
#33707=CARTESIAN_POINT('Ctrl Pts',(-7.83746246318038,0.989853539891906,
26.4));
#33708=CARTESIAN_POINT('Ctrl Pts',(-7.80179749749225,0.959976425281334,
26.4));
#33709=CARTESIAN_POINT('Ctrl Pts',(-7.79470173084572,0.954032187588742,
26.4));
#33710=CARTESIAN_POINT('Ctrl Pts',(-7.78767071045979,0.948000723246587,
26.4));
#33711=CARTESIAN_POINT('Ctrl Pts',(-7.78071179729939,0.941887340642186,
26.4));
#33712=CARTESIAN_POINT('Ctrl Pts',(-7.75269360207171,0.917273447155726,
26.4));
#33713=CARTESIAN_POINT('Ctrl Pts',(-7.72591293956663,0.891394850496869,
26.4));
#33714=CARTESIAN_POINT('Ctrl Pts',(-7.70047126076455,0.864315910058709,
26.4));
#33715=CARTESIAN_POINT('Ctrl Pts',(-7.66652682771193,0.82818703318742,26.4));
#33716=CARTESIAN_POINT('Ctrl Pts',(-7.63496397922782,0.78992201446398,26.4));
#33717=CARTESIAN_POINT('Ctrl Pts',(-7.60593250072696,0.749787089159704,
26.4));
#33718=CARTESIAN_POINT('Ctrl Pts',(-7.58573725869745,0.721867927883357,
26.4));
#33719=CARTESIAN_POINT('Ctrl Pts',(-7.56676781226386,0.693043181405103,
26.4));
#33720=CARTESIAN_POINT('Ctrl Pts',(-7.54908829087147,0.663396724297125,
26.4));
#33721=CARTESIAN_POINT('Ctrl Pts',(-7.53965742741635,0.647582286637428,
26.4));
#33722=CARTESIAN_POINT('Ctrl Pts',(-7.53059381571656,0.631533970667596,
26.4));
#33723=CARTESIAN_POINT('Ctrl Pts',(-7.52190863960029,0.615264252922367,
26.4));
#33724=CARTESIAN_POINT('Ctrl Pts',(-7.51748928486193,0.606985588995857,
26.4));
#33725=CARTESIAN_POINT('Ctrl Pts',(-7.51316793018883,0.598649598701858,
26.4));
#33726=CARTESIAN_POINT('Ctrl Pts',(-7.508946155198,0.590257920257115,26.4));
#33727=CARTESIAN_POINT('Ctrl Pts',(-7.50442378911426,0.581268752888771,
26.4));
#33728=CARTESIAN_POINT('Ctrl Pts',(-7.50001905759358,0.572222229998695,
26.4));
#33729=CARTESIAN_POINT('Ctrl Pts',(-7.49573669483179,0.563127939236245,
26.4));
#33730=CARTESIAN_POINT('Ctrl Pts',(-7.47506542038098,0.519229140665572,
26.4));
#33731=CARTESIAN_POINT('Ctrl Pts',(-7.45721490167107,0.474166034199356,
26.4));
#33732=CARTESIAN_POINT('Ctrl Pts',(-7.44233264532585,0.428186070859631,
26.4));
#33733=CARTESIAN_POINT('Ctrl Pts',(-7.43702167377983,0.411777384480363,
26.4));
#33734=CARTESIAN_POINT('Ctrl Pts',(-7.4320891762645,0.39525178308813,26.4));
#33735=CARTESIAN_POINT('Ctrl Pts',(-7.42754343216099,0.378620146479998,
26.4));
#33736=CARTESIAN_POINT('Ctrl Pts',(-7.41562255541274,0.335004913063347,
26.4));
#33737=CARTESIAN_POINT('Ctrl Pts',(-7.40635865253341,0.290660154332935,
26.4));
#33738=CARTESIAN_POINT('Ctrl Pts',(-7.39978193143838,0.245833148209606,
26.4));
#33739=CARTESIAN_POINT('Ctrl Pts',(-7.39701831329359,0.226996295360151,
26.4));
#33740=CARTESIAN_POINT('Ctrl Pts',(-7.39472966852691,0.208074337051025,
26.4));
#33741=CARTESIAN_POINT('Ctrl Pts',(-7.39292029821568,0.189086061607282,
26.4));
#33742=CARTESIAN_POINT('Ctrl Pts',(-7.39203040388929,0.179747144924149,
26.4));
#33743=CARTESIAN_POINT('Ctrl Pts',(-7.39125632551953,0.170390221780269,
26.4));
#33744=CARTESIAN_POINT('Ctrl Pts',(-7.3905991129645,0.161023830066182,26.4));
#33745=CARTESIAN_POINT('Ctrl Pts',(-7.38726308367779,0.113479764101907,
26.4));
#33746=CARTESIAN_POINT('Ctrl Pts',(-7.38694582795301,0.0658794268722831,
26.4));
#33747=CARTESIAN_POINT('Ctrl Pts',(-7.38964467812272,0.0185117250965961,
26.4));
#33748=CARTESIAN_POINT('Ctrl Pts',(-7.39231294873441,-0.028319272789147,
26.4));
#33749=CARTESIAN_POINT('Ctrl Pts',(-7.39792954447875,-0.0749239502970285,
26.4));
#33750=CARTESIAN_POINT('Ctrl Pts',(-7.40654136040071,-0.121014043924224,
26.4));
#33751=CARTESIAN_POINT('Ctrl Pts',(-7.40892324964069,-0.13376181966341,
26.4));
#33752=CARTESIAN_POINT('Ctrl Pts',(-7.41153455473596,-0.146470124525479,
26.4));
#33753=CARTESIAN_POINT('Ctrl Pts',(-7.41437692003386,-0.159132568267465,
26.4));
#33754=CARTESIAN_POINT('Ctrl Pts',(-7.41931563096904,-0.181134015238621,
26.4));
#33755=CARTESIAN_POINT('Ctrl Pts',(-7.42495181516823,-0.202997104027968,
26.4));
#33756=CARTESIAN_POINT('Ctrl Pts',(-7.43127552851572,-0.224690029431199,
26.4));
#33757=CARTESIAN_POINT('Ctrl Pts',(-7.43448552072453,-0.235701616722459,
26.4));
#33758=CARTESIAN_POINT('Ctrl Pts',(-7.43787270196213,-0.246669331595252,
26.4));
#33759=CARTESIAN_POINT('Ctrl Pts',(-7.44143596905709,-0.257588833328584,
26.4));
#33760=CARTESIAN_POINT('Ctrl Pts',(-7.44466453004633,-0.267482640438386,
26.4));
#33761=CARTESIAN_POINT('Ctrl Pts',(-7.44803504929267,-0.277328758820201,
26.4));
#33762=CARTESIAN_POINT('Ctrl Pts',(-7.4515445537233,-0.287120147614807,
26.4));
#33763=CARTESIAN_POINT('Ctrl Pts',(-7.46731925100687,-0.331130975147226,
26.4));
#33764=CARTESIAN_POINT('Ctrl Pts',(-7.48590735102023,-0.374065461792036,
26.4));
#33765=CARTESIAN_POINT('Ctrl Pts',(-7.50719015735612,-0.415648998792841,
26.4));
#33766=CARTESIAN_POINT('Ctrl Pts',(-7.51904253208635,-0.438806831240468,
26.4));
#33767=CARTESIAN_POINT('Ctrl Pts',(-7.53173142467898,-0.461545209553912,
26.4));
#33768=CARTESIAN_POINT('Ctrl Pts',(-7.54524163262262,-0.483812028629736,
26.4));
#33769=CARTESIAN_POINT('Ctrl Pts',(-7.55097536126223,-0.493262060692935,
26.4));
#33770=CARTESIAN_POINT('Ctrl Pts',(-7.55685648518396,-0.502625914171693,
26.4));
#33771=CARTESIAN_POINT('Ctrl Pts',(-7.56287699180982,-0.511889479160034,
26.4));
#33772=CARTESIAN_POINT('Ctrl Pts',(-7.58817006364992,-0.550807136644064,
26.4));
#33773=CARTESIAN_POINT('Ctrl Pts',(-7.61595022831774,-0.588008141121294,
26.4));
#33774=CARTESIAN_POINT('Ctrl Pts',(-7.64611613239271,-0.62320527942628,
26.4));
#33775=CARTESIAN_POINT('Ctrl Pts',(-7.66532276604225,-0.645615300331212,
26.4));
#33776=CARTESIAN_POINT('Ctrl Pts',(-7.6854974434774,-0.667212207978329,
26.4));
#33777=CARTESIAN_POINT('Ctrl Pts',(-7.70658042403511,-0.687941803185361,
26.4));
#33778=CARTESIAN_POINT('Ctrl Pts',(-7.70661869325989,-0.687936125025681,
25.2));
#33779=CARTESIAN_POINT('Ctrl Pts',(-7.67409908369756,-0.655902484444094,
25.2));
#33780=CARTESIAN_POINT('Ctrl Pts',(-7.64381552971734,-0.621809035232042,
25.2));
#33781=CARTESIAN_POINT('Ctrl Pts',(-7.61585836477246,-0.585955246406357,
25.2));
#33782=CARTESIAN_POINT('Ctrl Pts',(-7.58750223492001,-0.549589803284789,
25.2));
#33783=CARTESIAN_POINT('Ctrl Pts',(-7.56153863793393,-0.511412632439867,
25.2));
#33784=CARTESIAN_POINT('Ctrl Pts',(-7.53809218129987,-0.471690967864502,
25.2));
#33785=CARTESIAN_POINT('Ctrl Pts',(-7.51733028405296,-0.436517332408129,
25.2));
#33786=CARTESIAN_POINT('Ctrl Pts',(-7.49854222357723,-0.400131575643489,
25.2));
#33787=CARTESIAN_POINT('Ctrl Pts',(-7.48184098880052,-0.362698062471297,
25.2));
#33788=CARTESIAN_POINT('Ctrl Pts',(-7.47711369552762,-0.352102486912628,
25.2));
#33789=CARTESIAN_POINT('Ctrl Pts',(-7.47255243649911,-0.341419159457484,
25.2));
#33790=CARTESIAN_POINT('Ctrl Pts',(-7.46817016271403,-0.330677368055269,
25.2));
#33791=CARTESIAN_POINT('Ctrl Pts',(-7.45707013423535,-0.303469074752666,
25.2));
#33792=CARTESIAN_POINT('Ctrl Pts',(-7.44710388175771,-0.275856356158202,
25.2));
#33793=CARTESIAN_POINT('Ctrl Pts',(-7.43829878902219,-0.247907854317032,
25.2));
#33794=CARTESIAN_POINT('Ctrl Pts',(-7.42417917490964,-0.203090375061034,
25.2));
#33795=CARTESIAN_POINT('Ctrl Pts',(-7.4130426814431,-0.157410581164318,
25.2));
#33796=CARTESIAN_POINT('Ctrl Pts',(-7.40485403128444,-0.111171922541295,
25.2));
#33797=CARTESIAN_POINT('Ctrl Pts',(-7.39906737058042,-0.078496521385322,
25.2));
#33798=CARTESIAN_POINT('Ctrl Pts',(-7.39475376399804,-0.0455412949444171,
25.2));
#33799=CARTESIAN_POINT('Ctrl Pts',(-7.39191539897434,-0.0124075347941399,
25.2));
#33800=CARTESIAN_POINT('Ctrl Pts',(-7.39015663071979,0.00812351213599617,
25.2));
#33801=CARTESIAN_POINT('Ctrl Pts',(-7.38896453092616,0.0287231847245958,
25.2));
#33802=CARTESIAN_POINT('Ctrl Pts',(-7.38834204837582,0.0493677427878705,
25.2));
#33803=CARTESIAN_POINT('Ctrl Pts',(-7.38797993275816,0.0613772632001962,
25.2));
#33804=CARTESIAN_POINT('Ctrl Pts',(-7.38781079076705,0.0734063969638433,
25.2));
#33805=CARTESIAN_POINT('Ctrl Pts',(-7.38783494145012,0.0854216419247253,
25.2));
#33806=CARTESIAN_POINT('Ctrl Pts',(-7.38793210908909,0.133763669381329,
25.2));
#33807=CARTESIAN_POINT('Ctrl Pts',(-7.39114956164653,0.181962052576744,
25.2));
#33808=CARTESIAN_POINT('Ctrl Pts',(-7.39745513654038,0.229705853778749,
25.2));
#33809=CARTESIAN_POINT('Ctrl Pts',(-7.39993171457249,0.248457712446122,
25.2));
#33810=CARTESIAN_POINT('Ctrl Pts',(-7.40288520968687,0.267139634278219,
25.2));
#33811=CARTESIAN_POINT('Ctrl Pts',(-7.40631580517995,0.285733272919791,
25.2));
#33812=CARTESIAN_POINT('Ctrl Pts',(-7.41475571884804,0.331477140195014,
25.2));
#33813=CARTESIAN_POINT('Ctrl Pts',(-7.42608006767679,0.376687101444302,
25.2));
#33814=CARTESIAN_POINT('Ctrl Pts',(-7.44015868375257,0.421133147358343,
25.2));
#33815=CARTESIAN_POINT('Ctrl Pts',(-7.44619887655232,0.44020197380139,25.2));
#33816=CARTESIAN_POINT('Ctrl Pts',(-7.45274661951137,0.459130118611719,
25.2));
#33817=CARTESIAN_POINT('Ctrl Pts',(-7.45979413108642,0.477898840262571,
25.2));
#33818=CARTESIAN_POINT('Ctrl Pts',(-7.46424294742261,0.489746794622125,
25.2));
#33819=CARTESIAN_POINT('Ctrl Pts',(-7.46889308133366,0.501535927254051,
25.2));
#33820=CARTESIAN_POINT('Ctrl Pts',(-7.47373049342834,0.513232826928775,
25.2));
#33821=CARTESIAN_POINT('Ctrl Pts',(-7.49246868158931,0.558541910115242,
25.2));
#33822=CARTESIAN_POINT('Ctrl Pts',(-7.51403763849658,0.60254052436522,25.2));
#33823=CARTESIAN_POINT('Ctrl Pts',(-7.5382574080668,0.644974713240491,25.2));
#33824=CARTESIAN_POINT('Ctrl Pts',(-7.56269829320146,0.687796307107259,
25.2));
#33825=CARTESIAN_POINT('Ctrl Pts',(-7.58983893767671,0.729025863014533,
25.2));
#33826=CARTESIAN_POINT('Ctrl Pts',(-7.61954528866539,0.768390684532343,
25.2));
#33827=CARTESIAN_POINT('Ctrl Pts',(-7.6249432342603,0.775543672288655,25.2));
#33828=CARTESIAN_POINT('Ctrl Pts',(-7.63042602246557,0.782635032671784,
25.2));
#33829=CARTESIAN_POINT('Ctrl Pts',(-7.63599301409741,0.789663044280778,
25.2));
#33830=CARTESIAN_POINT('Ctrl Pts',(-7.65117037049777,0.808823597058622,
25.2));
#33831=CARTESIAN_POINT('Ctrl Pts',(-7.66697341498186,0.827513438421461,
25.2));
#33832=CARTESIAN_POINT('Ctrl Pts',(-7.68337390615606,0.845711906332443,
25.2));
#33833=CARTESIAN_POINT('Ctrl Pts',(-7.69112608445907,0.854313951636385,
25.2));
#33834=CARTESIAN_POINT('Ctrl Pts',(-7.69901178372298,0.862806182343179,
25.2));
#33835=CARTESIAN_POINT('Ctrl Pts',(-7.70702820259955,0.871186249340306,
25.2));
#33836=CARTESIAN_POINT('Ctrl Pts',(-7.71445585235118,0.878950838929277,
25.2));
#33837=CARTESIAN_POINT('Ctrl Pts',(-7.72199001781368,0.886613096267017,
25.2));
#33838=CARTESIAN_POINT('Ctrl Pts',(-7.72962411164412,0.89416783589762,25.2));
#33839=CARTESIAN_POINT('Ctrl Pts',(-7.76528208932064,0.929455159197961,
25.2));
#33840=CARTESIAN_POINT('Ctrl Pts',(-7.80314201059037,0.962425606050914,
25.2));
#33841=CARTESIAN_POINT('Ctrl Pts',(-7.84293252810485,0.992923651767303,
25.2));
#33842=CARTESIAN_POINT('Ctrl Pts',(-7.86518031888562,1.0099758084796,25.2));
#33843=CARTESIAN_POINT('Ctrl Pts',(-7.88803247402863,1.02625455224781,25.2));
#33844=CARTESIAN_POINT('Ctrl Pts',(-7.9114469066033,1.04172808762183,25.2));
#33845=CARTESIAN_POINT('Ctrl Pts',(-7.92363425798135,1.04978215479012,25.2));
#33846=CARTESIAN_POINT('Ctrl Pts',(-7.93597623364268,1.05761914082858,25.2));
#33847=CARTESIAN_POINT('Ctrl Pts',(-7.94844679456435,1.06522236279636,25.2));
#33848=CARTESIAN_POINT('Ctrl Pts',(-7.99400675878279,1.09299998426606,25.2));
#33849=CARTESIAN_POINT('Ctrl Pts',(-8.04133383320788,1.11769842594191,25.2));
#33850=CARTESIAN_POINT('Ctrl Pts',(-8.09012873835892,1.13911714460503,25.2));
#33851=CARTESIAN_POINT('Ctrl Pts',(-8.1212439149797,1.1527752757589,25.2));
#33852=CARTESIAN_POINT('Ctrl Pts',(-8.15295691405469,1.16509895636455,25.2));
#33853=CARTESIAN_POINT('Ctrl Pts',(-8.18517804880577,1.17607982959758,25.2));
#33854=CARTESIAN_POINT('Ctrl Pts',(-9.5501656695242,-1.36966039699926E-5,
25.6841069671524));
#33855=CARTESIAN_POINT('Ctrl Pts',(-9.55006298344665,0.154119342427657,
25.6770974504288));
#33856=CARTESIAN_POINT('Ctrl Pts',(-9.515673521871,0.308296731012387,25.6700879337053));
#33857=CARTESIAN_POINT('Ctrl Pts',(-9.44996669084627,0.447714404793194,
25.6630784169817));
#33858=CARTESIAN_POINT('Ctrl Pts',(-9.37761882318798,0.601223123059134,
25.6553604433654));
#33859=CARTESIAN_POINT('Ctrl Pts',(-9.26730313198972,0.736837801786184,
25.647642469749));
#33860=CARTESIAN_POINT('Ctrl Pts',(-9.13173841581746,0.838922806907227,
25.6399244961327));
#33861=CARTESIAN_POINT('Ctrl Pts',(-8.99617369964519,0.941007812028272,
25.6322065225163));
#33862=CARTESIAN_POINT('Ctrl Pts',(-8.83535995849891,1.00956314354331,25.6244885488999));
#33863=CARTESIAN_POINT('Ctrl Pts',(-8.66783814118664,1.03668474492625,25.6167705752836));
#33864=CARTESIAN_POINT('Ctrl Pts',(-8.50031632387437,1.06380634630919,25.6090526016672));
#33865=CARTESIAN_POINT('Ctrl Pts',(-8.3260864303961,1.04949421756004,25.6013346280509));
#33866=CARTESIAN_POINT('Ctrl Pts',(-8.16523621882741,0.995398469324722,
25.5936166544345));
#33867=CARTESIAN_POINT('Ctrl Pts',(-8.00438600725873,0.941302721089401,
25.5858986808181));
#33868=CARTESIAN_POINT('Ctrl Pts',(-7.85691547759961,0.847423353367908,
25.5781807072018));
#33869=CARTESIAN_POINT('Ctrl Pts',(-7.73982717908252,0.724584145853212,
25.5704627335854));
#33870=CARTESIAN_POINT('Ctrl Pts',(-7.62273888056543,0.601744938338516,
25.562744759969));
#33871=CARTESIAN_POINT('Ctrl Pts',(-7.53603281319035,0.449945891030617,
25.5550267863527));
#33872=CARTESIAN_POINT('Ctrl Pts',(-7.48970571428075,0.28668860819909,25.5473088127363));
#33873=CARTESIAN_POINT('Ctrl Pts',(-7.44337861537115,0.123431325367562,
25.5395908391199));
#33874=CARTESIAN_POINT('Ctrl Pts',(-7.43743048492702,-0.0512841929875971,
25.5318728655036));
#33875=CARTESIAN_POINT('Ctrl Pts',(-7.47254711037184,-0.217314200152739,
25.5241548918872));
#33876=CARTESIAN_POINT('Ctrl Pts',(-7.50766373581667,-0.383344207317882,
25.5164369182709));
#33877=CARTESIAN_POINT('Ctrl Pts',(-7.58384511715045,-0.540688703293009,
25.5087189446545));
#33878=CARTESIAN_POINT('Ctrl Pts',(-7.69230795508232,-0.671206721513239,
25.5010009710381));
#33879=CARTESIAN_POINT('Ctrl Pts',(-7.80077079301418,-0.801724739733468,
25.4932829974218));
#33880=CARTESIAN_POINT('Ctrl Pts',(-7.94151508754413,-0.9054162801988,25.4855650238054));
#33881=CARTESIAN_POINT('Ctrl Pts',(-8.0983137895737,-0.97032627906681,25.4778470501891));
#33882=CARTESIAN_POINT('Ctrl Pts',(-8.25511249160327,-1.03523627793482,
25.4701290765727));
#33883=CARTESIAN_POINT('Ctrl Pts',(-8.42796560113247,-1.06136473520551,
25.4624111029563));
#33884=CARTESIAN_POINT('Ctrl Pts',(-8.59694409194747,-1.04569916835105,
25.45469312934));
#33885=CARTESIAN_POINT('Ctrl Pts',(-8.76592258276247,-1.0300336014966,25.4469751557236));
#33886=CARTESIAN_POINT('Ctrl Pts',(-8.93102645486326,-0.972574010516992,
25.4392571821072));
#33887=CARTESIAN_POINT('Ctrl Pts',(-9.07322013923887,-0.879945203081139,
25.4315392084909));
#33888=CARTESIAN_POINT('Ctrl Pts',(-9.21541382361448,-0.787316395645285,
25.4238212348745));
#33889=CARTESIAN_POINT('Ctrl Pts',(-9.33469732026492,-0.659518371753182,
25.4161032612582));
#33890=CARTESIAN_POINT('Ctrl Pts',(-9.41731787352031,-0.511285482216741,
25.4083852876418));
#33891=CARTESIAN_POINT('Ctrl Pts',(-9.4999384267757,-0.3630525926803,25.4006673140254));
#33892=CARTESIAN_POINT('Ctrl Pts',(-9.54589603663603,-0.19438483749952,
25.3929493404091));
#33893=CARTESIAN_POINT('Ctrl Pts',(-9.54989208229683,-0.0247288318319217,
25.3852313667927));
#33894=CARTESIAN_POINT('Ctrl Pts',(-9.55008613808259,-0.0164900046805863,
25.3848565669126));
#33895=CARTESIAN_POINT('Ctrl Pts',(-9.55018123744808,-0.00824884697431659,
25.3844817670325));
#33896=CARTESIAN_POINT('Ctrl Pts',(-9.55017788167088,-7.61182092967605E-6,
25.3841069671524));
#33897=CARTESIAN_POINT('Ctrl Pts',(-8.8147888955044,1.17604951161383,25.2));
#33898=CARTESIAN_POINT('Ctrl Pts',(-9.00489125583826,1.12516550422186,25.2077179736164));
#33899=CARTESIAN_POINT('Ctrl Pts',(-9.35978529202387,0.929507318017654,
25.2231539208491));
#33900=CARTESIAN_POINT('Ctrl Pts',(-9.69399227712924,0.421517236998932,
25.2463078416982));
#33901=CARTESIAN_POINT('Ctrl Pts',(-9.75281486267965,-0.183635718934528,
25.2694617625473));
#33902=CARTESIAN_POINT('Ctrl Pts',(-9.52277787696657,-0.746472135969,25.2926156833964));
#33903=CARTESIAN_POINT('Ctrl Pts',(-9.05688673586305,-1.13717144686837,
25.3157696042454));
#33904=CARTESIAN_POINT('Ctrl Pts',(-8.46258910686823,-1.26565668871267,
25.3389235250945));
#33905=CARTESIAN_POINT('Ctrl Pts',(-7.87691540315674,-1.10229327660247,
25.3620774459436));
#33906=CARTESIAN_POINT('Ctrl Pts',(-7.43491939071853,-0.684754086769719,
25.3852313667927));
#33907=CARTESIAN_POINT('Ctrl Pts',(-7.23851882542848,-0.109317624216872,
25.4083852876418));
#33908=CARTESIAN_POINT('Ctrl Pts',(-7.3330023279845,0.49132607864821,25.4315392084909));
#33909=CARTESIAN_POINT('Ctrl Pts',(-7.69658267289797,0.978675431042071,
25.45469312934));
#33910=CARTESIAN_POINT('Ctrl Pts',(-8.24542235634912,1.24035284195992,25.477847050189));
#33911=CARTESIAN_POINT('Ctrl Pts',(-8.85296484867377,1.21601841356867,25.5010009710381));
#33912=CARTESIAN_POINT('Ctrl Pts',(-9.37911750114581,0.911283371272776,
25.5241548918872));
#33913=CARTESIAN_POINT('Ctrl Pts',(-9.70255522576049,0.396416310789831,
25.5473088127363));
#33914=CARTESIAN_POINT('Ctrl Pts',(-9.7486968123668,-0.209860036229624,
25.5704627335854));
#33915=CARTESIAN_POINT('Ctrl Pts',(-9.50690251025353,-0.767744943225855,
25.5936166544345));
#33916=CARTESIAN_POINT('Ctrl Pts',(-9.03292745405576,-1.14859622679878,
25.6167705752836));
#33917=CARTESIAN_POINT('Ctrl Pts',(-8.4360651298626,-1.26459372752363,25.6399244961327));
#33918=CARTESIAN_POINT('Ctrl Pts',(-7.85394549062537,-1.08898968511111,
25.6630784169818));
#33919=CARTESIAN_POINT('Ctrl Pts',(-7.42079898622258,-0.662276479442534,
25.6862323378308));
#33920=CARTESIAN_POINT('Ctrl Pts',(-7.23650448403929,-0.0828495292575919,
25.7093862586799));
#33921=CARTESIAN_POINT('Ctrl Pts',(-7.34355828943908,0.515681620221391,
25.732540179529));
#33922=CARTESIAN_POINT('Ctrl Pts',(-7.71727496063508,0.995302203406518,
25.7556941003781));
#33923=CARTESIAN_POINT('Ctrl Pts',(-8.27147950269888,1.24541693647946,25.7788480212272));
#33924=CARTESIAN_POINT('Ctrl Pts',(-8.878378383048,1.20835208552723,25.8020019420763));
#33925=CARTESIAN_POINT('Ctrl Pts',(-9.39802732848356,0.892654401575867,
25.8251558629253));
#33926=CARTESIAN_POINT('Ctrl Pts',(-9.71060095072233,0.371120332865739,
25.8483097837744));
#33927=CARTESIAN_POINT('Ctrl Pts',(-9.74402317613577,-0.235990043419514,
25.8714637046235));
#33928=CARTESIAN_POINT('Ctrl Pts',(-9.49058720348329,-0.788683685422225,
25.8946176254726));
#33929=CARTESIAN_POINT('Ctrl Pts',(-9.00873260835677,-1.15951545765943,
25.9177715463217));
#33930=CARTESIAN_POINT('Ctrl Pts',(-8.40956981340752,-1.26297559149317,
25.9409254671708));
#33931=CARTESIAN_POINT('Ctrl Pts',(-7.83125923477822,-1.07520730665756,
25.9640793880199));
#33932=CARTESIAN_POINT('Ctrl Pts',(-7.40715299459429,-0.63950792499141,
25.987233308869));
#33933=CARTESIAN_POINT('Ctrl Pts',(-7.2350453736822,-0.056344979529684,
26.0103872297181));
#33934=CARTESIAN_POINT('Ctrl Pts',(-7.35462251532982,0.539810504688725,
26.0335411505671));
#33935=CARTESIAN_POINT('Ctrl Pts',(-7.73831123274286,1.0114915645451,26.0566950714162));
#33936=CARTESIAN_POINT('Ctrl Pts',(-8.29763708577969,1.24993368402129,26.0798489922653));
#33937=CARTESIAN_POINT('Ctrl Pts',(-8.90362562319939,1.20015470640273,26.1030029131144));
#33938=CARTESIAN_POINT('Ctrl Pts',(-9.41654248721522,0.873633122741245,
26.1261568339635));
#33939=CARTESIAN_POINT('Ctrl Pts',(-9.71811463367633,0.345661252800576,
26.1493107548126));
#33940=CARTESIAN_POINT('Ctrl Pts',(-9.73880281063852,-0.262016335241189,
26.1724646756617));
#33941=CARTESIAN_POINT('Ctrl Pts',(-9.47383654720263,-0.809275815695625,
26.1956185965107));
#33942=CARTESIAN_POINT('Ctrl Pts',(-8.98431418402503,-1.16992509177172,
26.2187725173598));
#33943=CARTESIAN_POINT('Ctrl Pts',(-8.38311423523835,-1.26080241069298,
26.2419264382089));
#33944=CARTESIAN_POINT('Ctrl Pts',(-7.80886688894933,-1.06095235748777,
26.265080359058));
#33945=CARTESIAN_POINT('Ctrl Pts',(-7.39398727066922,-0.616458384095017,
26.2882342799071));
#33946=CARTESIAN_POINT('Ctrl Pts',(-7.23414222788049,-0.0298155056950012,
26.3113882007562));
#33947=CARTESIAN_POINT('Ctrl Pts',(-7.36618999782964,0.563701837361564,
26.3345421216053));
#33948=CARTESIAN_POINT('Ctrl Pts',(-7.75968238765149,1.02723719824325,26.3576960424544));
#33949=CARTESIAN_POINT('Ctrl Pts',(-8.32388291100964,1.25389971972182,26.3808499633034));
#33950=CARTESIAN_POINT('Ctrl Pts',(-8.9286957354243,1.19143409461849,26.4040038841525));
#33951=CARTESIAN_POINT('Ctrl Pts',(-9.43465037119409,0.854222360422852,
26.4271578050016));
#33952=CARTESIAN_POINT('Ctrl Pts',(-9.72509064095728,0.320073835810339,
26.4503117258507));
#33953=CARTESIAN_POINT('Ctrl Pts',(-9.73300563867467,-0.287943914027406,
26.4734656466998));
#33954=CARTESIAN_POINT('Ctrl Pts',(-9.54874216054247,-0.648885562186029,
26.4889015939325));
#33955=CARTESIAN_POINT('Ctrl Pts',(-9.41981913331181,-0.797569598526366,
26.4966195675489));
#33956=CARTESIAN_POINT('Ctrl Pts',(-8.80036532666169,1.12216314098435,25.1677934774837));
#33957=CARTESIAN_POINT('Ctrl Pts',(-8.98175723208245,1.07361062937922,25.1755114511001));
#33958=CARTESIAN_POINT('Ctrl Pts',(-9.32039008931324,0.886917464999664,
25.1909473983328));
#33959=CARTESIAN_POINT('Ctrl Pts',(-9.63928377230971,0.402203395332122,
25.2141013191819));
#33960=CARTESIAN_POINT('Ctrl Pts',(-9.69541111789357,-0.175221564331685,
25.237255240031));
#33961=CARTESIAN_POINT('Ctrl Pts',(-9.47591438422618,-0.712268921065058,
25.2604091608801));
#33962=CARTESIAN_POINT('Ctrl Pts',(-9.03137028885039,-1.08506646195909,
25.2835630817291));
#33963=CARTESIAN_POINT('Ctrl Pts',(-8.46430326705704,-1.20766453383812,
25.3067170025782));
#33964=CARTESIAN_POINT('Ctrl Pts',(-7.90546502388907,-1.05178640298975,
25.3298709234273));
#33965=CARTESIAN_POINT('Ctrl Pts',(-7.48372118681235,-0.653378781440023,
25.3530248442764));
#33966=CARTESIAN_POINT('Ctrl Pts',(-7.29631965901905,-0.104308710938382,
25.3761787651255));
#33967=CARTESIAN_POINT('Ctrl Pts',(-7.38647394500143,0.468813608796805,
25.3993326859746));
#33968=CARTESIAN_POINT('Ctrl Pts',(-7.73339510590426,0.933832704199109,
25.4224866068237));
#33969=CARTESIAN_POINT('Ctrl Pts',(-8.25708705679266,1.18352010465326,25.4456405276728));
#33970=CARTESIAN_POINT('Ctrl Pts',(-8.83679206473314,1.16030067526026,25.4687944485218));
#33971=CARTESIAN_POINT('Ctrl Pts',(-9.33883650019663,0.869528536116644,
25.4919483693709));
#33972=CARTESIAN_POINT('Ctrl Pts',(-9.64745436822191,0.378252588909212,
25.51510229022));
#33973=CARTESIAN_POINT('Ctrl Pts',(-9.69148175588273,-0.200244288269261,
25.5382562110691));
#33974=CARTESIAN_POINT('Ctrl Pts',(-9.46076642387327,-0.732567012236534,
25.5614101319182));
#33975=CARTESIAN_POINT('Ctrl Pts',(-9.00850881689442,-1.09596776059079,
25.5845640527673));
#33976=CARTESIAN_POINT('Ctrl Pts',(-8.43899461376132,-1.20665027733373,
25.6077179736164));
#33977=CARTESIAN_POINT('Ctrl Pts',(-7.88354758849218,-1.03909237959457,
25.6308718944655));
#33978=CARTESIAN_POINT('Ctrl Pts',(-7.47024777663305,-0.631931093914118,
25.6540258153145));
#33979=CARTESIAN_POINT('Ctrl Pts',(-7.29439761437894,-0.0790533791840066,
25.6771797361636));
#33980=CARTESIAN_POINT('Ctrl Pts',(-7.39654623425882,0.492053183969649,
25.7003336570127));
#33981=CARTESIAN_POINT('Ctrl Pts',(-7.75313927685278,0.949697640935758,
25.7234875778618));
#33982=CARTESIAN_POINT('Ctrl Pts',(-8.28195026952663,1.18835216330059,25.7466414987109));
#33983=CARTESIAN_POINT('Ctrl Pts',(-8.861041155673,1.15298561694865,25.76979541956));
#33984=CARTESIAN_POINT('Ctrl Pts',(-9.35687988275089,0.851753142358179,
25.7929493404091));
#33985=CARTESIAN_POINT('Ctrl Pts',(-9.65513143955736,0.354115668004737,
25.8161032612581));
#33986=CARTESIAN_POINT('Ctrl Pts',(-9.68702226479751,-0.225177023373172,
25.8392571821072));
#33987=CARTESIAN_POINT('Ctrl Pts',(-9.44519868143504,-0.752546345146674,
25.8624111029563));
#33988=CARTESIAN_POINT('Ctrl Pts',(-8.98542257454059,-1.10638667431739,
25.8855650238054));
#33989=CARTESIAN_POINT('Ctrl Pts',(-8.41371330779504,-1.20510628399625,
25.9087189446545));
#33990=CARTESIAN_POINT('Ctrl Pts',(-7.86190081268282,-1.02594150716706,
25.9318728655036));
#33991=CARTESIAN_POINT('Ctrl Pts',(-7.45722704181174,-0.610205790407563,
25.9550267863527));
#33992=CARTESIAN_POINT('Ctrl Pts',(-7.29300536018796,-0.0537632630117455,
25.9781807072018));
#33993=CARTESIAN_POINT('Ctrl Pts',(-7.40710349937011,0.515076487423223,
26.0013346280509));
#33994=CARTESIAN_POINT('Ctrl Pts',(-7.77321167087187,0.965145208547828,
26.0244885488999));
#33995=CARTESIAN_POINT('Ctrl Pts',(-8.30690931699925,1.19266195430728,26.047642469749));
#33996=CARTESIAN_POINT('Ctrl Pts',(-8.88513157196049,1.14516384021616,26.0707963905981));
#33997=CARTESIAN_POINT('Ctrl Pts',(-9.37454668034144,0.833603414993973,
26.0939503114472));
#33998=CARTESIAN_POINT('Ctrl Pts',(-9.66230084695114,0.329823118269062,
26.1171042322963));
#33999=CARTESIAN_POINT('Ctrl Pts',(-9.68204109547968,-0.250010795327814,
26.1402581531454));
#34000=CARTESIAN_POINT('Ctrl Pts',(-9.42921553712026,-0.772194947827906,
26.1634120739945));
#34001=CARTESIAN_POINT('Ctrl Pts',(-8.96212299788553,-1.11631934092418,
26.1865659948435));
#34002=CARTESIAN_POINT('Ctrl Pts',(-8.38846991931377,-1.20303267793751,
26.2097199156926));
#34003=CARTESIAN_POINT('Ctrl Pts',(-7.84053447998916,-1.01233971712592,
26.2328738365417));
#34004=CARTESIAN_POINT('Ctrl Pts',(-7.44466456891651,-0.588212375202577,
26.2560277573908));
#34005=CARTESIAN_POINT('Ctrl Pts',(-7.29214359635947,-0.0284493647506621,
26.2791816782399));
#34006=CARTESIAN_POINT('Ctrl Pts',(-7.41814096196594,0.537873123661492,
26.302335599089));
#34007=CARTESIAN_POINT('Ctrl Pts',(-7.79360360342394,0.980169380228542,
26.3254895199381));
#34008=CARTESIAN_POINT('Ctrl Pts',(-8.3319525633821,1.19644626698716,26.3486434407871));
#34009=CARTESIAN_POINT('Ctrl Pts',(-8.90905297629025,1.13684280524742,26.3717973616362));
#34010=CARTESIAN_POINT('Ctrl Pts',(-9.39182486443287,0.815082050207028,
26.3949512824853));
#34011=CARTESIAN_POINT('Ctrl Pts',(-9.66895721487156,0.305408111982431,
26.4181052033344));
#34012=CARTESIAN_POINT('Ctrl Pts',(-9.67650954886066,-0.274750377259986,
26.4412591241835));
#34013=CARTESIAN_POINT('Ctrl Pts',(-9.50068898914138,-0.619153746004165,
26.4566950714162));
#34014=CARTESIAN_POINT('Ctrl Pts',(-9.37767319112124,-0.761025107359477,
26.4644130450326));
#34015=CARTESIAN_POINT('Ctrl Pts',(-8.78594175781898,1.06827677035487,25.1355869549674));
#34016=CARTESIAN_POINT('Ctrl Pts',(-8.95862320832664,1.02205575453657,25.1433049285838));
#34017=CARTESIAN_POINT('Ctrl Pts',(-9.2809948866026,0.844327611981674,25.1587408758165));
#34018=CARTESIAN_POINT('Ctrl Pts',(-9.58457526749019,0.382889553665313,
25.1818947966656));
#34019=CARTESIAN_POINT('Ctrl Pts',(-9.63800737310749,-0.166807409728842,
25.2050487175147));
#34020=CARTESIAN_POINT('Ctrl Pts',(-9.42905089148579,-0.678065706161117,
25.2282026383638));
#34021=CARTESIAN_POINT('Ctrl Pts',(-9.00585384183773,-1.0329614770498,25.2513565592128));
#34022=CARTESIAN_POINT('Ctrl Pts',(-8.46601742724585,-1.14967237896357,
25.2745104800619));
#34023=CARTESIAN_POINT('Ctrl Pts',(-7.9340146446214,-1.00127952937703,25.297664400911));
#34024=CARTESIAN_POINT('Ctrl Pts',(-7.53252298290617,-0.622003476110328,
25.3208183217601));
#34025=CARTESIAN_POINT('Ctrl Pts',(-7.35412049260963,-0.0992997976598917,
25.3439722426092));
#34026=CARTESIAN_POINT('Ctrl Pts',(-7.43994556201836,0.4463011389454,25.3671261634583));
#34027=CARTESIAN_POINT('Ctrl Pts',(-7.77020753891055,0.888989977356148,
25.3902800843074));
#34028=CARTESIAN_POINT('Ctrl Pts',(-8.2687517572362,1.12668736734659,25.4134340051565));
#34029=CARTESIAN_POINT('Ctrl Pts',(-8.82061928079252,1.10458293695185,25.4365879260056));
#34030=CARTESIAN_POINT('Ctrl Pts',(-9.29855549924744,0.827773700960511,
25.4597418468546));
#34031=CARTESIAN_POINT('Ctrl Pts',(-9.59235351068334,0.360088867028593,
25.4828957677037));
#34032=CARTESIAN_POINT('Ctrl Pts',(-9.63426669939866,-0.1906285403089,25.5060496885528));
#34033=CARTESIAN_POINT('Ctrl Pts',(-9.41463033749301,-0.697389081247213,
25.5292036094019));
#34034=CARTESIAN_POINT('Ctrl Pts',(-8.98409017973308,-1.04333929438279,
25.552357530251));
#34035=CARTESIAN_POINT('Ctrl Pts',(-8.44192409766004,-1.14870682714383,
25.5755114511001));
#34036=CARTESIAN_POINT('Ctrl Pts',(-7.91314968635899,-0.989195074078023,
25.5986653719492));
#34037=CARTESIAN_POINT('Ctrl Pts',(-7.51969656704351,-0.601585708385703,
25.6218192927982));
#34038=CARTESIAN_POINT('Ctrl Pts',(-7.35229074471859,-0.0752572291104221,
25.6449732136473));
#34039=CARTESIAN_POINT('Ctrl Pts',(-7.44953417907855,0.468424747717907,
25.6681271344964));
#34040=CARTESIAN_POINT('Ctrl Pts',(-7.78900359307048,0.904093078464998,
25.6912810553455));
#34041=CARTESIAN_POINT('Ctrl Pts',(-8.29242103635439,1.13128739012173,25.7144349761946));
#34042=CARTESIAN_POINT('Ctrl Pts',(-8.843703928298,1.09761914837007,25.7375888970437));
#34043=CARTESIAN_POINT('Ctrl Pts',(-9.31573243701821,0.810851883140491,
25.7607428178928));
#34044=CARTESIAN_POINT('Ctrl Pts',(-9.59966192839239,0.337111003143734,
25.7838967387419));
#34045=CARTESIAN_POINT('Ctrl Pts',(-9.63002135345923,-0.21436400332683,
25.8070506595909));
#34046=CARTESIAN_POINT('Ctrl Pts',(-9.39981015938679,-0.716409004871123,
25.83020458044));
#34047=CARTESIAN_POINT('Ctrl Pts',(-8.96211254072442,-1.05325789097535,
25.8533585012891));
#34048=CARTESIAN_POINT('Ctrl Pts',(-8.41785680218255,-1.14723697649933,
25.8765124221382));
#34049=CARTESIAN_POINT('Ctrl Pts',(-7.89254239058742,-0.976675707676555,
25.8996663429873));
#34050=CARTESIAN_POINT('Ctrl Pts',(-7.50730108902919,-0.580903655823716,
25.9228202638364));
#34051=CARTESIAN_POINT('Ctrl Pts',(-7.35096534669371,-0.051181546493807,
25.9459741846855));
#34052=CARTESIAN_POINT('Ctrl Pts',(-7.4595844834104,0.49034247015772,25.9691281055346));
#34053=CARTESIAN_POINT('Ctrl Pts',(-7.80811210900088,0.91879885255056,25.9922820263836));
#34054=CARTESIAN_POINT('Ctrl Pts',(-8.31618154821881,1.13539022459327,26.0154359472327));
#34055=CARTESIAN_POINT('Ctrl Pts',(-8.86663752072159,1.0901729740296,26.0385898680818));
#34056=CARTESIAN_POINT('Ctrl Pts',(-9.33255087346766,0.793573707246701,
26.0617437889309));
#34057=CARTESIAN_POINT('Ctrl Pts',(-9.60648706022596,0.313984983737547,
26.08489770978));
#34058=CARTESIAN_POINT('Ctrl Pts',(-9.62527938032086,-0.23800525541444,
26.1080516306291));
#34059=CARTESIAN_POINT('Ctrl Pts',(-9.38459452703789,-0.735114079960188,
26.1312055514782));
#34060=CARTESIAN_POINT('Ctrl Pts',(-8.93993181174604,-1.06271359007664,
26.1543594723272));
#34061=CARTESIAN_POINT('Ctrl Pts',(-8.39382560338919,-1.14526294518203,
26.1775133931763));
#34062=CARTESIAN_POINT('Ctrl Pts',(-7.87220207102899,-0.963727076764081,
26.2006673140254));
#34063=CARTESIAN_POINT('Ctrl Pts',(-7.49534186716381,-0.559966366310139,
26.2238212348745));
#34064=CARTESIAN_POINT('Ctrl Pts',(-7.35014496483845,-0.0270832238063217,
26.2469751557236));
#34065=CARTESIAN_POINT('Ctrl Pts',(-7.47009192610224,0.51204440996142,26.2701290765727));
#34066=CARTESIAN_POINT('Ctrl Pts',(-7.8275248191964,0.933101562213838,26.2932829974218));
#34067=CARTESIAN_POINT('Ctrl Pts',(-8.34002221575455,1.1389928142525,26.3164369182709));
#34068=CARTESIAN_POINT('Ctrl Pts',(-8.8894102171562,1.08225151587636,26.3395908391199));
#34069=CARTESIAN_POINT('Ctrl Pts',(-9.34899935767165,0.775941739991204,
26.362744759969));
#34070=CARTESIAN_POINT('Ctrl Pts',(-9.61282378878583,0.290742388154523,
26.3858986808181));
#34071=CARTESIAN_POINT('Ctrl Pts',(-9.62001345904665,-0.261556840492567,
26.4090526016672));
#34072=CARTESIAN_POINT('Ctrl Pts',(-9.45263581774029,-0.5894219298223,26.4244885488999));
#34073=CARTESIAN_POINT('Ctrl Pts',(-9.33552724893067,-0.724480616192588,
26.4322065225163));
#34074=CARTESIAN_POINT('Ctrl Pts',(-8.77151818897628,1.01439039972539,25.1033804324511));
#34075=CARTESIAN_POINT('Ctrl Pts',(-8.93548918457083,0.970500879693931,
25.1110984060675));
#34076=CARTESIAN_POINT('Ctrl Pts',(-9.24159968389196,0.801737758963685,
25.1265343533002));
#34077=CARTESIAN_POINT('Ctrl Pts',(-9.52986676267067,0.363575711998503,
25.1496882741493));
#34078=CARTESIAN_POINT('Ctrl Pts',(-9.5806036283214,-0.158393255125999,
25.1728421949984));
#34079=CARTESIAN_POINT('Ctrl Pts',(-9.38218739874541,-0.643862491257174,
25.1959961158475));
#34080=CARTESIAN_POINT('Ctrl Pts',(-8.98033739482507,-0.980856492140519,
25.2191500366966));
#34081=CARTESIAN_POINT('Ctrl Pts',(-8.46773158743466,-1.09168022408902,
25.2423039575456));
#34082=CARTESIAN_POINT('Ctrl Pts',(-7.96256426535373,-0.950772655764307,
25.2654578783947));
#34083=CARTESIAN_POINT('Ctrl Pts',(-7.58132477899998,-0.590628170780633,
25.2886117992438));
#34084=CARTESIAN_POINT('Ctrl Pts',(-7.41192132620021,-0.0942908843814014,
25.3117657200929));
#34085=CARTESIAN_POINT('Ctrl Pts',(-7.4934171790353,0.423788669093995,25.334919640942));
#34086=CARTESIAN_POINT('Ctrl Pts',(-7.80701997191684,0.844147250513186,
25.3580735617911));
#34087=CARTESIAN_POINT('Ctrl Pts',(-8.28041645767974,1.06985463003993,25.3812274826402));
#34088=CARTESIAN_POINT('Ctrl Pts',(-8.80444649685189,1.04886519864344,25.4043814034892));
#34089=CARTESIAN_POINT('Ctrl Pts',(-9.25827449829825,0.78601886580438,25.4275353243384));
#34090=CARTESIAN_POINT('Ctrl Pts',(-9.53725265314477,0.341925145147974,
25.4506892451874));
#34091=CARTESIAN_POINT('Ctrl Pts',(-9.5770516429146,-0.181012792348538,
25.4738431660365));
#34092=CARTESIAN_POINT('Ctrl Pts',(-9.36849425111276,-0.662211150257891,
25.4969970868856));
#34093=CARTESIAN_POINT('Ctrl Pts',(-8.95967154257173,-0.990710828174794,
25.5201510077347));
#34094=CARTESIAN_POINT('Ctrl Pts',(-8.44485358155876,-1.09076337695393,
25.5433049285838));
#34095=CARTESIAN_POINT('Ctrl Pts',(-7.9427517842258,-0.93929776856148,25.5664588494329));
#34096=CARTESIAN_POINT('Ctrl Pts',(-7.56914535745397,-0.571240322857287,
25.5896127702819));
#34097=CARTESIAN_POINT('Ctrl Pts',(-7.41018387505824,-0.0714610790368369,
25.612766691131));
#34098=CARTESIAN_POINT('Ctrl Pts',(-7.50252212389829,0.444796311466165,
25.6359206119801));
#34099=CARTESIAN_POINT('Ctrl Pts',(-7.82486790928818,0.858488515994237,
25.6590745328292));
#34100=CARTESIAN_POINT('Ctrl Pts',(-8.30289180318214,1.07422261694286,25.6822284536783));
#34101=CARTESIAN_POINT('Ctrl Pts',(-8.826366700923,1.04225267979148,25.7053823745274));
#34102=CARTESIAN_POINT('Ctrl Pts',(-9.27458499128554,0.769950623922804,
25.7285362953765));
#34103=CARTESIAN_POINT('Ctrl Pts',(-9.54419241722742,0.320106338282732,
25.7516902162256));
#34104=CARTESIAN_POINT('Ctrl Pts',(-9.57302044212097,-0.203550983280489,
25.7748441370746));
#34105=CARTESIAN_POINT('Ctrl Pts',(-9.35442163733854,-0.680271664595571,
25.7979980579237));
#34106=CARTESIAN_POINT('Ctrl Pts',(-8.93880250690824,-1.00012910763331,
25.8211519787728));
#34107=CARTESIAN_POINT('Ctrl Pts',(-8.42200029657007,-1.08936766900241,
25.8443058996219));
#34108=CARTESIAN_POINT('Ctrl Pts',(-7.92318396849201,-0.92740990818605,
25.867459820471));
#34109=CARTESIAN_POINT('Ctrl Pts',(-7.55737513624663,-0.551601521239869,
25.8906137413201));
#34110=CARTESIAN_POINT('Ctrl Pts',(-7.40892533319946,-0.0485998299758685,
25.9137676621692));
#34111=CARTESIAN_POINT('Ctrl Pts',(-7.51206546745069,0.465608452892217,
25.9369215830183));
#34112=CARTESIAN_POINT('Ctrl Pts',(-7.84301254712989,0.872452496553292,
25.9600755038674));
#34113=CARTESIAN_POINT('Ctrl Pts',(-8.32545377943837,1.07811849487926,25.9832294247164));
#34114=CARTESIAN_POINT('Ctrl Pts',(-8.84814346948268,1.03518210784304,26.0063833455655));
#34115=CARTESIAN_POINT('Ctrl Pts',(-9.29055506659387,0.753543999499429,
26.0295372664146));
#34116=CARTESIAN_POINT('Ctrl Pts',(-9.55067327350077,0.298146849206033,
26.0526911872637));
#34117=CARTESIAN_POINT('Ctrl Pts',(-9.56851766516202,-0.225999715501066,
26.0758451081128));
#34118=CARTESIAN_POINT('Ctrl Pts',(-9.33997351695551,-0.698033212092468,
26.0989990289619));
#34119=CARTESIAN_POINT('Ctrl Pts',(-8.91774062560654,-1.00910783922911,
26.1221529498109));
#34120=CARTESIAN_POINT('Ctrl Pts',(-8.39918128746461,-1.08749321242655,
26.14530687066));
#34121=CARTESIAN_POINT('Ctrl Pts',(-7.90386966206882,-0.915114436402238,
26.1684607915091));
#34122=CARTESIAN_POINT('Ctrl Pts',(-7.5460191654111,-0.531720357417699,
26.1916147123582));
#34123=CARTESIAN_POINT('Ctrl Pts',(-7.40814633331743,-0.0257170828619826,
26.2147686332073));
#34124=CARTESIAN_POINT('Ctrl Pts',(-7.52204289023854,0.486215696261348,
26.2379225540564));
#34125=CARTESIAN_POINT('Ctrl Pts',(-7.86144603496885,0.886033744199133,
26.2610764749055));
#34126=CARTESIAN_POINT('Ctrl Pts',(-8.34809186812701,1.08153936151783,26.2842303957546));
#34127=CARTESIAN_POINT('Ctrl Pts',(-8.86976745802214,1.0276602265053,26.3073843166036));
#34128=CARTESIAN_POINT('Ctrl Pts',(-9.30617385091043,0.73680142977538,26.3305382374527));
#34129=CARTESIAN_POINT('Ctrl Pts',(-9.55669036270011,0.276076664326615,
26.3536921583018));
#34130=CARTESIAN_POINT('Ctrl Pts',(-9.56351736923264,-0.248363303725146,
26.3768460791509));
#34131=CARTESIAN_POINT('Ctrl Pts',(-9.40458264633919,-0.559690113640436,
26.3922820263836));
#34132=CARTESIAN_POINT('Ctrl Pts',(-9.2933813067401,-0.687936125025699,
26.4));
#34133=CARTESIAN_POINT('Ctrl Pts',(-9.2933813067401,-0.687936125025699,
26.4));
#34134=CARTESIAN_POINT('Ctrl Pts',(-9.3259008940156,-0.655902506397881,
26.4));
#34135=CARTESIAN_POINT('Ctrl Pts',(-9.35618442453939,-0.621809077591114,
26.4));
#34136=CARTESIAN_POINT('Ctrl Pts',(-9.38414156706932,-0.585955309047688,
26.4));
#34137=CARTESIAN_POINT('Ctrl Pts',(-9.41249768479717,-0.549589872890676,
26.4));
#34138=CARTESIAN_POINT('Ctrl Pts',(-9.43846126893405,-0.511412707527682,
26.4));
#34139=CARTESIAN_POINT('Ctrl Pts',(-9.46190771414193,-0.471691048741587,
26.4));
#34140=CARTESIAN_POINT('Ctrl Pts',(-9.48266961930019,-0.436517387867455,
26.4));
#34141=CARTESIAN_POINT('Ctrl Pts',(-9.50145768537511,-0.400131603820207,
26.4));
#34142=CARTESIAN_POINT('Ctrl Pts',(-9.51815892464979,-0.362698063167964,
26.4));
#34143=CARTESIAN_POINT('Ctrl Pts',(-9.52288622415338,-0.352102468719386,
26.4));
#34144=CARTESIAN_POINT('Ctrl Pts',(-9.52744748898763,-0.341419122144753,
26.4));
#34145=CARTESIAN_POINT('Ctrl Pts',(-9.53182976813775,-0.330677311537023,
26.4));
#34146=CARTESIAN_POINT('Ctrl Pts',(-9.54292979396936,-0.303469009386603,
26.4));
#34147=CARTESIAN_POINT('Ctrl Pts',(-9.55289604429056,-0.275856282583612,
26.4));
#34148=CARTESIAN_POINT('Ctrl Pts',(-9.5617011358392,-0.247907773694988,
26.4));
#34149=CARTESIAN_POINT('Ctrl Pts',(-9.57582075051757,-0.203090275300733,
26.4));
#34150=CARTESIAN_POINT('Ctrl Pts',(-9.58695724599474,-0.157410464943264,
26.4));
#34151=CARTESIAN_POINT('Ctrl Pts',(-9.59514589843678,-0.111171791667601,
26.4));
#34152=CARTESIAN_POINT('Ctrl Pts',(-9.60093255826271,-0.0784963942267053,
26.4));
#34153=CARTESIAN_POINT('Ctrl Pts',(-9.60524616537179,-0.045541172645693,
26.4));
#34154=CARTESIAN_POINT('Ctrl Pts',(-9.6080845319163,-0.0124074180728123,
26.4));
#34155=CARTESIAN_POINT('Ctrl Pts',(-9.6098433032337,0.00812365015497431,
26.4));
#34156=CARTESIAN_POINT('Ctrl Pts',(-9.61103540510615,0.028723343930919,
26.4));
#34157=CARTESIAN_POINT('Ctrl Pts',(-9.61165788864374,0.0493679230858363,
26.4));
#34158=CARTESIAN_POINT('Ctrl Pts',(-9.61202000347441,0.0613774106196558,
26.4));
#34159=CARTESIAN_POINT('Ctrl Pts',(-9.6121891457594,0.0734065113012894,
26.4));
#34160=CARTESIAN_POINT('Ctrl Pts',(-9.61216499643434,0.0854217231952467,
26.4));
#34161=CARTESIAN_POINT('Ctrl Pts',(-9.61206783397847,0.133763757288094,
26.4));
#34162=CARTESIAN_POINT('Ctrl Pts',(-9.60885038574432,0.181962146521315,
26.4));
#34163=CARTESIAN_POINT('Ctrl Pts',(-9.60254481310853,0.22970595413251,26.4));
#34164=CARTESIAN_POINT('Ctrl Pts',(-9.60006823815714,0.248457798706134,
26.4));
#34165=CARTESIAN_POINT('Ctrl Pts',(-9.59711474664968,0.267139706625319,
26.4));
#34166=CARTESIAN_POINT('Ctrl Pts',(-9.59368415521716,0.28573333164128,26.4));
#34167=CARTESIAN_POINT('Ctrl Pts',(-9.58524424594579,0.331477195708921,
26.4));
#34168=CARTESIAN_POINT('Ctrl Pts',(-9.57391990043447,0.376687154779727,
26.4));
#34169=CARTESIAN_POINT('Ctrl Pts',(-9.55984128692189,0.42113319919065,26.4));
#34170=CARTESIAN_POINT('Ctrl Pts',(-9.55380109519868,0.440202025061907,
26.4));
#34171=CARTESIAN_POINT('Ctrl Pts',(-9.54725335317324,0.459130169423877,
26.4));
#34172=CARTESIAN_POINT('Ctrl Pts',(-9.54020584241397,0.47789889072224,26.4));
#34173=CARTESIAN_POINT('Ctrl Pts',(-9.53575702659671,0.489746844848731,
26.4));
#34174=CARTESIAN_POINT('Ctrl Pts',(-9.53110689315819,0.501535977285736,
26.4));
#34175=CARTESIAN_POINT('Ctrl Pts',(-9.52626948149497,0.513232876797037,
26.4));
#34176=CARTESIAN_POINT('Ctrl Pts',(-9.50753129667904,0.558541955303412,
26.4));
#34177=CARTESIAN_POINT('Ctrl Pts',(-9.48596234301021,0.602540565578701,
26.4));
#34178=CARTESIAN_POINT('Ctrl Pts',(-9.46174257689923,0.644974750847517,
26.4));
#34179=CARTESIAN_POINT('Ctrl Pts',(-9.43730169352057,0.687796344114401,
26.4));
#34180=CARTESIAN_POINT('Ctrl Pts',(-9.41016105064264,0.729025899571633,
26.4));
#34181=CARTESIAN_POINT('Ctrl Pts',(-9.3804547014595,0.768390720401401,26.4));
#34182=CARTESIAN_POINT('Ctrl Pts',(-9.3750567531779,0.775543712027657,26.4));
#34183=CARTESIAN_POINT('Ctrl Pts',(-9.36957396219805,0.782635076204051,
26.4));
#34184=CARTESIAN_POINT('Ctrl Pts',(-9.36400696770699,0.789663091524419,
26.4));
#34185=CARTESIAN_POINT('Ctrl Pts',(-9.3488296116131,0.808823644192825,26.4));
#34186=CARTESIAN_POINT('Ctrl Pts',(-9.33302656747451,0.827513485340246,
26.4));
#34187=CARTESIAN_POINT('Ctrl Pts',(-9.31662607666973,0.845711952950721,
26.4));
#34188=CARTESIAN_POINT('Ctrl Pts',(-9.308873897103,0.854313999708652,26.4));
#34189=CARTESIAN_POINT('Ctrl Pts',(-9.30098819653116,0.862806231809669,
26.4));
#34190=CARTESIAN_POINT('Ctrl Pts',(-9.29297177630242,0.87118630014213,26.4));
#34191=CARTESIAN_POINT('Ctrl Pts',(-9.28554412806376,0.878950888077058,
26.4));
#34192=CARTESIAN_POINT('Ctrl Pts',(-9.27800996416404,0.886613143777747,
26.4));
#34193=CARTESIAN_POINT('Ctrl Pts',(-9.27037587193287,0.894167881801814,
26.4));
#34194=CARTESIAN_POINT('Ctrl Pts',(-9.23471789561382,0.929455203647225,
26.4));
#34195=CARTESIAN_POINT('Ctrl Pts',(-9.19685797580996,0.96242564884392,26.4));
#34196=CARTESIAN_POINT('Ctrl Pts',(-9.15706745972836,0.992923692890463,
26.4));
#34197=CARTESIAN_POINT('Ctrl Pts',(-9.13481966941932,1.00997584892161,26.4));
#34198=CARTESIAN_POINT('Ctrl Pts',(-9.11196751471993,1.02625459198139,26.4));
#34199=CARTESIAN_POINT('Ctrl Pts',(-9.08855308253825,1.04172812665066,26.4));
#34200=CARTESIAN_POINT('Ctrl Pts',(-9.07636573164392,1.04978219326764,26.4));
#34201=CARTESIAN_POINT('Ctrl Pts',(-9.06402375646026,1.0576191787653,26.4));
#34202=CARTESIAN_POINT('Ctrl Pts',(-9.05155319600525,1.06522240020876,26.4));
#34203=CARTESIAN_POINT('Ctrl Pts',(-9.0059932331111,1.09300001999494,26.4));
#34204=CARTESIAN_POINT('Ctrl Pts',(-8.95866615983379,1.11769846015436,26.4));
#34205=CARTESIAN_POINT('Ctrl Pts',(-8.90987125549013,1.13911717768622,26.4));
#34206=CARTESIAN_POINT('Ctrl Pts',(-8.87875607920242,1.15277530819852,26.4));
#34207=CARTESIAN_POINT('Ctrl Pts',(-8.84704308031516,1.16509898830357,26.4));
#34208=CARTESIAN_POINT('Ctrl Pts',(-8.81482194563461,1.17607986114086,26.4));
#34209=CARTESIAN_POINT('Ctrl Pts',(-9.55005314880761,-1.91003690738122E-5,
25.4658930328476));
#34210=CARTESIAN_POINT('Ctrl Pts',(-9.55009383677427,-0.0583092511807032,
25.4685430772439));
#34211=CARTESIAN_POINT('Ctrl Pts',(-9.5453163970275,-0.116592801535466,
25.4711931216402));
#34212=CARTESIAN_POINT('Ctrl Pts',(-9.53565891265265,-0.174056195750679,
25.4738431660365));
#34213=CARTESIAN_POINT('Ctrl Pts',(-9.50753251231398,-0.34141224498499,
25.4815611396529));
#34214=CARTESIAN_POINT('Ctrl Pts',(-9.43801338171337,-0.50181169762144,
25.4892791132692));
#34215=CARTESIAN_POINT('Ctrl Pts',(-9.33511669832289,-0.636761370259148,
25.4969970868856));
#34216=CARTESIAN_POINT('Ctrl Pts',(-9.23222001493242,-0.771711042896858,
25.504715060502));
#34217=CARTESIAN_POINT('Ctrl Pts',(-9.09594577875207,-0.881210935535826,
25.5124330341183));
#34218=CARTESIAN_POINT('Ctrl Pts',(-8.94200566715974,-0.952636306651832,
25.5201510077347));
#34219=CARTESIAN_POINT('Ctrl Pts',(-8.78806555556741,-1.02406167776784,
25.527868981351));
#34220=CARTESIAN_POINT('Ctrl Pts',(-8.61645956856308,-1.05741252736088,
25.5355869549674));
#34221=CARTESIAN_POINT('Ctrl Pts',(-8.4469729421721,-1.048843684092,25.5433049285838));
#34222=CARTESIAN_POINT('Ctrl Pts',(-8.27748631578111,-1.04027484082311,
25.5510229022001));
#34223=CARTESIAN_POINT('Ctrl Pts',(-8.11011905000345,-0.989786304692296,
25.5587408758165));
#34224=CARTESIAN_POINT('Ctrl Pts',(-7.96416767931932,-0.903199129009522,
25.5664588494329));
#34225=CARTESIAN_POINT('Ctrl Pts',(-7.81821630863519,-0.816611953326749,
25.5741768230492));
#34226=CARTESIAN_POINT('Ctrl Pts',(-7.69368083304458,-0.693926138092018,
25.5818947966656));
#34227=CARTESIAN_POINT('Ctrl Pts',(-7.60491951484999,-0.54928668983791,
25.589612770282));
#34228=CARTESIAN_POINT('Ctrl Pts',(-7.51615819665539,-0.404647241583803,
25.5973307438983));
#34229=CARTESIAN_POINT('Ctrl Pts',(-7.46317103585682,-0.23805416031032,
25.6050487175147));
#34230=CARTESIAN_POINT('Ctrl Pts',(-7.45206716359754,-0.0687147212564117,
25.612766691131));
#34231=CARTESIAN_POINT('Ctrl Pts',(-7.44096329133826,0.100624717797497,
25.6204846647474));
#34232=CARTESIAN_POINT('Ctrl Pts',(-7.47174270761827,0.272710514631827,
25.6282026383638));
#34233=CARTESIAN_POINT('Ctrl Pts',(-7.54085671332326,0.427702113803672,
25.6359206119801));
#34234=CARTESIAN_POINT('Ctrl Pts',(-7.60997071902825,0.582693712975518,
25.6436385855965));
#34235=CARTESIAN_POINT('Ctrl Pts',(-7.71741931415822,0.72059111448488,25.6513565592129));
#34236=CARTESIAN_POINT('Ctrl Pts',(-7.85081426070553,0.825495498730995,
25.6590745328292));
#34237=CARTESIAN_POINT('Ctrl Pts',(-7.98420920725284,0.930399882977112,
25.6667925064456));
#34238=CARTESIAN_POINT('Ctrl Pts',(-8.14355050521749,1.00231124995999,25.6745104800619));
#34239=CARTESIAN_POINT('Ctrl Pts',(-8.31046697048996,1.03293861059286,25.6822284536783));
#34240=CARTESIAN_POINT('Ctrl Pts',(-8.47738343576243,1.06356597122573,25.6899464272947));
#34241=CARTESIAN_POINT('Ctrl Pts',(-8.65187506834272,1.05290932550861,25.697664400911));
#34242=CARTESIAN_POINT('Ctrl Pts',(-8.81382393302662,1.00219732667193,25.7053823745274));
#34243=CARTESIAN_POINT('Ctrl Pts',(-8.97577279771052,0.951485327835256,
25.7131003481437));
#34244=CARTESIAN_POINT('Ctrl Pts',(-9.12517889449803,0.860717975879029,
25.7208183217601));
#34245=CARTESIAN_POINT('Ctrl Pts',(-9.2448165138821,0.740360252294236,25.7285362953765));
#34246=CARTESIAN_POINT('Ctrl Pts',(-9.36445413326617,0.620002528709445,
25.7362542689928));
#34247=CARTESIAN_POINT('Ctrl Pts',(-9.45432327524679,0.470054433496088,
25.7439722426092));
#34248=CARTESIAN_POINT('Ctrl Pts',(-9.5040625170527,0.307804165628874,25.7516902162256));
#34249=CARTESIAN_POINT('Ctrl Pts',(-9.53457300099597,0.208278438801921,
25.7564244884329));
#34250=CARTESIAN_POINT('Ctrl Pts',(-9.54998379775559,0.104123770513768,
25.7611587606403));
#34251=CARTESIAN_POINT('Ctrl Pts',(-9.55003919466624,-1.48519393190782E-5,
25.7658930328476));
#34252=CARTESIAN_POINT('Ctrl Pts',(-8.8147888955044,1.17604951161383,25.2));
#34253=CARTESIAN_POINT('Ctrl Pts',(-8.86280020341074,1.15963879009472,25.2));
#34254=CARTESIAN_POINT('Ctrl Pts',(-8.90960731244362,1.14022121906871,25.2));
#34255=CARTESIAN_POINT('Ctrl Pts',(-8.95497238860795,1.11798779738799,25.2));
#34256=CARTESIAN_POINT('Ctrl Pts',(-9.00031600398345,1.09576489363885,25.2));
#34257=CARTESIAN_POINT('Ctrl Pts',(-9.04421984864658,1.07072810229581,25.2));
#34258=CARTESIAN_POINT('Ctrl Pts',(-9.08641918731652,1.04302391286584,25.2));
#34259=CARTESIAN_POINT('Ctrl Pts',(-9.12519792826817,1.01756537206777,25.2));
#34260=CARTESIAN_POINT('Ctrl Pts',(-9.1625375171365,0.989853465475151,25.2));
#34261=CARTESIAN_POINT('Ctrl Pts',(-9.19820248282102,0.959976338255365,
25.2));
#34262=CARTESIAN_POINT('Ctrl Pts',(-9.2052982498248,0.954032097754221,25.2));
#34263=CARTESIAN_POINT('Ctrl Pts',(-9.21232927057154,0.948000630658807,
25.2));
#34264=CARTESIAN_POINT('Ctrl Pts',(-9.21928818410342,0.94188724537333,25.2));
#34265=CARTESIAN_POINT('Ctrl Pts',(-9.24730637906229,0.917273342642342,
25.2));
#34266=CARTESIAN_POINT('Ctrl Pts',(-9.27408704155894,0.891394738150684,
25.2));
#34267=CARTESIAN_POINT('Ctrl Pts',(-9.29952872082846,0.864315792473915,
25.2));
#34268=CARTESIAN_POINT('Ctrl Pts',(-9.33347315480174,0.828186908297136,
25.2));
#34269=CARTESIAN_POINT('Ctrl Pts',(-9.36503600501172,0.789921886846104,
25.2));
#34270=CARTESIAN_POINT('Ctrl Pts',(-9.39406748567017,0.749786961749021,
25.2));
#34271=CARTESIAN_POINT('Ctrl Pts',(-9.41426272810871,0.72186780212627,25.2));
#34272=CARTESIAN_POINT('Ctrl Pts',(-9.4332321752929,0.693043058821335,25.2));
#34273=CARTESIAN_POINT('Ctrl Pts',(-9.4509116976612,0.663396605844021,25.2));
#34274=CARTESIAN_POINT('Ctrl Pts',(-9.46034256416092,0.647582166155294,
25.2));
#34275=CARTESIAN_POINT('Ctrl Pts',(-9.4694061787729,0.631533848303631,25.2));
#34276=CARTESIAN_POINT('Ctrl Pts',(-9.47809135764204,0.615264128747603,
25.2));
#34277=CARTESIAN_POINT('Ctrl Pts',(-9.48251070130078,0.606985487278882,
25.2));
#34278=CARTESIAN_POINT('Ctrl Pts',(-9.48683204540646,0.598649519784842,
25.2));
#34279=CARTESIAN_POINT('Ctrl Pts',(-9.4910538103519,0.590257864458163,25.2));
#34280=CARTESIAN_POINT('Ctrl Pts',(-9.49557618446465,0.581268684505481,
25.2));
#34281=CARTESIAN_POINT('Ctrl Pts',(-9.4999809236823,0.572222148823553,25.2));
#34282=CARTESIAN_POINT('Ctrl Pts',(-9.50426329374563,0.563127845164782,
25.2));
#34283=CARTESIAN_POINT('Ctrl Pts',(-9.52493457020396,0.519229054928066,
25.2));
#34284=CARTESIAN_POINT('Ctrl Pts',(-9.54278509116266,0.474165957397592,
25.2));
#34285=CARTESIAN_POINT('Ctrl Pts',(-9.55766734967247,0.42818600198001,25.2));
#34286=CARTESIAN_POINT('Ctrl Pts',(-9.5629783230983,0.411777315006687,25.2));
#34287=CARTESIAN_POINT('Ctrl Pts',(-9.56791082232496,0.395251712842571,
25.2));
#34288=CARTESIAN_POINT('Ctrl Pts',(-9.57245656795131,0.378620075217546,
25.2));
#34289=CARTESIAN_POINT('Ctrl Pts',(-9.58437744649104,0.335004847190819,
25.2));
#34290=CARTESIAN_POINT('Ctrl Pts',(-9.59364135084807,0.290660092434833,
25.2));
#34291=CARTESIAN_POINT('Ctrl Pts',(-9.60021807317259,0.245833089310576,
25.2));
#34292=CARTESIAN_POINT('Ctrl Pts',(-9.60298169195186,0.226996236918194,
25.2));
#34293=CARTESIAN_POINT('Ctrl Pts',(-9.60527033726867,0.208074278886572,
25.2));
#34294=CARTESIAN_POINT('Ctrl Pts',(-9.60707970804988,0.189086003575891,
25.2));
#34295=CARTESIAN_POINT('Ctrl Pts',(-9.60796960254794,0.179747087582501,
25.2));
#34296=CARTESIAN_POINT('Ctrl Pts',(-9.60874368108558,0.170390165094709,
25.2));
#34297=CARTESIAN_POINT('Ctrl Pts',(-9.60940089380497,0.161023774009816,
25.2));
#34298=CARTESIAN_POINT('Ctrl Pts',(-9.61273692395369,0.11347971084424,25.2));
#34299=CARTESIAN_POINT('Ctrl Pts',(-9.61305418040214,0.0658793756383451,
25.2));
#34300=CARTESIAN_POINT('Ctrl Pts',(-9.61035533089854,0.0185116756316162,
25.2));
#34301=CARTESIAN_POINT('Ctrl Pts',(-9.60768706096201,-0.0283193202137848,
25.2));
#34302=CARTESIAN_POINT('Ctrl Pts',(-9.602070465873,-0.0749239959345515,
25.2));
#34303=CARTESIAN_POINT('Ctrl Pts',(-9.59345865066658,-0.121014087532771,
25.2));
#34304=CARTESIAN_POINT('Ctrl Pts',(-9.59107676135001,-0.133761864179878,
25.2));
#34305=CARTESIAN_POINT('Ctrl Pts',(-9.58846545612991,-0.146470169922223,
25.2));
#34306=CARTESIAN_POINT('Ctrl Pts',(-9.5856230906601,-0.159132614503963,
25.2));
#34307=CARTESIAN_POINT('Ctrl Pts',(-9.58068437982785,-0.181134061145071,
25.2));
#34308=CARTESIAN_POINT('Ctrl Pts',(-9.57504819570294,-0.20299714950449,
25.2));
#34309=CARTESIAN_POINT('Ctrl Pts',(-9.56872448240039,-0.224690074400913,
25.2));
#34310=CARTESIAN_POINT('Ctrl Pts',(-9.56551448953387,-0.235701663769357,
25.2));
#34311=CARTESIAN_POINT('Ctrl Pts',(-9.56212730755587,-0.246669380680947,
25.2));
#34312=CARTESIAN_POINT('Ctrl Pts',(-9.55856403963841,-0.257588884414899,
25.2));
#34313=CARTESIAN_POINT('Ctrl Pts',(-9.55533547929827,-0.267482689064466,
25.2));
#34314=CARTESIAN_POINT('Ctrl Pts',(-9.55196496076087,-0.277328804982544,
25.2));
#34315=CARTESIAN_POINT('Ctrl Pts',(-9.5484554570926,-0.287120191330713,
25.2));
#34316=CARTESIAN_POINT('Ctrl Pts',(-9.5326807598597,-0.331131017285632,
25.2));
#34317=CARTESIAN_POINT('Ctrl Pts',(-9.5140926598038,-0.374065502137421,
25.2));
#34318=CARTESIAN_POINT('Ctrl Pts',(-9.49280985332475,-0.415649037346325,
25.2));
#34319=CARTESIAN_POINT('Ctrl Pts',(-9.48095747832615,-0.438806869164606,
25.2));
#34320=CARTESIAN_POINT('Ctrl Pts',(-9.46826858540731,-0.461545246835699,
25.2));
#34321=CARTESIAN_POINT('Ctrl Pts',(-9.45475837707871,-0.483812065291647,
25.2));
#34322=CARTESIAN_POINT('Ctrl Pts',(-9.44902464840965,-0.493262096871042,
25.2));
#34323=CARTESIAN_POINT('Ctrl Pts',(-9.44314352445654,-0.502625949871307,
25.2));
#34324=CARTESIAN_POINT('Ctrl Pts',(-9.43712301779533,-0.511889514393272,
25.2));
#34325=CARTESIAN_POINT('Ctrl Pts',(-9.41182994658654,-0.550807168718137,
25.2));
#34326=CARTESIAN_POINT('Ctrl Pts',(-9.38404978263737,-0.588008170344988,
25.2));
#34327=CARTESIAN_POINT('Ctrl Pts',(-9.35388387934858,-0.623205306360306,
25.2));
#34328=CARTESIAN_POINT('Ctrl Pts',(-9.33467724557846,-0.645615326532135,
25.2));
#34329=CARTESIAN_POINT('Ctrl Pts',(-9.3145025679876,-0.667212233621307,
25.2));
#34330=CARTESIAN_POINT('Ctrl Pts',(-9.29341958724169,-0.68794182840578,
25.2));
#34331=CARTESIAN_POINT('Origin',(-8.5,0.,26.4));
#34332=CARTESIAN_POINT('',(-7.46076951545867,-1.8,26.4));
#34333=CARTESIAN_POINT('',(-6.42153903091735,0.,26.4));
#34334=CARTESIAN_POINT('',(-7.46076951545867,-1.8,26.4));
#34335=CARTESIAN_POINT('',(-7.46076951545867,1.8,26.4));
#34336=CARTESIAN_POINT('',(-6.42153903091735,0.,26.4));
#34337=CARTESIAN_POINT('',(-9.53923048454133,1.8,26.4));
#34338=CARTESIAN_POINT('',(-7.46076951545867,1.8,26.4));
#34339=CARTESIAN_POINT('',(-10.5784609690827,2.22044604925031E-16,26.4));
#34340=CARTESIAN_POINT('',(-9.53923048454133,1.8,26.4));
#34341=CARTESIAN_POINT('',(-9.53923048454133,-1.8,26.4));
#34342=CARTESIAN_POINT('',(-10.5784609690827,2.54538057293978E-16,26.4));
#34343=CARTESIAN_POINT('',(-9.53923048454133,-1.8,26.4));
#34344=CARTESIAN_POINT('Origin',(-8.5,0.,25.1));
#34345=CARTESIAN_POINT('Origin',(-9.53923048454133,-1.8,25.2));
#34346=CARTESIAN_POINT('',(-9.53923048454133,-1.8,25.2));
#34347=CARTESIAN_POINT('',(-7.46076951545867,-1.8,25.2));
#34348=CARTESIAN_POINT('',(-9.53923048454133,-1.8,25.2));
#34349=CARTESIAN_POINT('',(-7.46076951545867,-1.8,25.2));
#34350=CARTESIAN_POINT('',(-9.53923048454133,-1.8,25.2));
#34351=CARTESIAN_POINT('Origin',(-10.5784609690827,2.54538057293978E-16,
25.2));
#34352=CARTESIAN_POINT('',(-10.5784609690827,2.54538057293978E-16,25.2));
#34353=CARTESIAN_POINT('',(-10.5784609690827,2.54538057293978E-16,25.2));
#34354=CARTESIAN_POINT('',(-10.5784609690827,2.54538057293978E-16,25.2));
#34355=CARTESIAN_POINT('Origin',(-9.53923048454133,1.8,25.2));
#34356=CARTESIAN_POINT('',(-9.53923048454133,1.8,25.2));
#34357=CARTESIAN_POINT('',(-9.53923048454133,1.8,25.2));
#34358=CARTESIAN_POINT('',(-9.53923048454133,1.8,25.2));
#34359=CARTESIAN_POINT('Origin',(-7.46076951545867,1.8,25.2));
#34360=CARTESIAN_POINT('',(-7.46076951545867,1.8,25.2));
#34361=CARTESIAN_POINT('',(-7.46076951545867,1.8,25.2));
#34362=CARTESIAN_POINT('',(-7.46076951545867,1.8,25.2));
#34363=CARTESIAN_POINT('Origin',(-6.42153903091735,0.,25.2));
#34364=CARTESIAN_POINT('',(-6.42153903091735,0.,25.2));
#34365=CARTESIAN_POINT('',(-6.42153903091735,0.,25.2));
#34366=CARTESIAN_POINT('',(-6.42153903091735,0.,25.2));
#34367=CARTESIAN_POINT('Origin',(-7.46076951545867,-1.8,25.2));
#34368=CARTESIAN_POINT('',(-7.46076951545867,-1.8,25.2));
#34369=CARTESIAN_POINT('Origin',(-8.5,0.,25.2));
#34403=UNCERTAINTY_MEASURE_WITH_UNIT(LENGTH_MEASURE(0.001),#34434,
'DISTANCE_ACCURACY_VALUE',
'Maximum model space distance between geometric entities at asserted c
onnectivities');
#34404=UNCERTAINTY_MEASURE_WITH_UNIT(LENGTH_MEASURE(0.001),#34434,
'DISTANCE_ACCURACY_VALUE',
'Maximum model space distance between geometric entities at asserted c
onnectivities');
#34432=(
GEOMETRIC_REPRESENTATION_CONTEXT(3)
GLOBAL_UNCERTAINTY_ASSIGNED_CONTEXT((#34403))
GLOBAL_UNIT_ASSIGNED_CONTEXT((#34434,#34436,#34437))
REPRESENTATION_CONTEXT('','3D')
);
#34433=(
GEOMETRIC_REPRESENTATION_CONTEXT(3)
GLOBAL_UNCERTAINTY_ASSIGNED_CONTEXT((#34404))
GLOBAL_UNIT_ASSIGNED_CONTEXT((#34434,#34436,#34437))
REPRESENTATION_CONTEXT('','3D')
);
#34434=(
LENGTH_UNIT()
NAMED_UNIT(*)
SI_UNIT(.CENTI.,.METRE.)
);
#34436=(
NAMED_UNIT(*)
PLANE_ANGLE_UNIT()
SI_UNIT($,.RADIAN.)
);
#34437=(
NAMED_UNIT(*)
SI_UNIT($,.STERADIAN.)
SOLID_ANGLE_UNIT()
);
#34465=SHAPE_DEFINITION_REPRESENTATION(#34530,#34564);
#34530=PRODUCT_DEFINITION_SHAPE('',$,#34593);
#34564=SHAPE_REPRESENTATION('',(#9696),#34432);
#34565=PRODUCT_DEFINITION_CONTEXT('part definition',#34651,'design');
#34593=PRODUCT_DEFINITION('M24 adjustment nut (3)',
'M24 adjustment nut (3)',#34621,#34565);
#34621=PRODUCT_DEFINITION_FORMATION('',$,#34680);
#34651=APPLICATION_CONTEXT(
'Core Data for Automotive Mechanical Design Process');
#34652=PRODUCT_CONTEXT('part definition',#34651,'mechanical');
#34680=PRODUCT('M24 adjustment nut (3)','M24 adjustment nut (3)',
'M24 adjustment nut (3)',(#34652));
#34744=COLOUR_RGB('Black',0.12,0.14,0.17);
#34745=FILL_AREA_STYLE_COLOUR('',#34744);
#34746=FILL_AREA_STYLE('',(#34745));
#34747=SURFACE_STYLE_FILL_AREA(#34746);
#34748=SURFACE_SIDE_STYLE('',(#34747));
#34749=SURFACE_STYLE_USAGE(.BOTH.,#34748);
#34750=PRESENTATION_STYLE_ASSIGNMENT((#34749));
ENDSEC;
END-ISO-10303-21;
